ISO-10303-21;
HEADER;
FILE_DESCRIPTION (('STEP AP214'),
    '1' );
FILE_NAME ('Servo-Body.step',
    '2026-11-01T06:29:40',
    ( '' ),
    ( '' ),
    'SwSTEP 2.0',
    'SolidWorks 2024',
    '' );
FILE_SCHEMA (( 'AUTOMOTIVE_DESIGN' ));
ENDSEC;

DATA;
#6=AXIS2_PLACEMENT_3D ( 'NONE', #11999, #10445, #9105 ) ;
#20=LINE ( 'NONE', #3221, #19065 ) ;
#62=EDGE_CURVE ( 'NONE', #13882, #666, #19278, .T. ) ;
#78=CARTESIAN_POINT ( 'NONE',  ( 37.00000000000000000, 0.000000000000000000, -23.00000000000000000 ) ) ;
#111=AXIS2_PLACEMENT_3D ( 'NONE', #18474, #20009, #10456 ) ;
#118=ORIENTED_EDGE ( 'NONE', *, *, #16621, .F. ) ;
#133=VECTOR ( 'NONE', #9166, 1000.000000000000000 ) ;
#137=AXIS2_PLACEMENT_3D ( 'NONE', #11998, #18269, #4176 ) ;
#154=CARTESIAN_POINT ( 'NONE',  ( -22.99999999999999645, 68.00000000000000000, -36.99999999999999289 ) ) ;
#197=ORIENTED_EDGE ( 'NONE', *, *, #17192, .T. ) ;
#240=ORIENTED_EDGE ( 'NONE', *, *, #2391, .T. ) ;
#242=CARTESIAN_POINT ( 'NONE',  ( -22.99999999999999645, 0.000000000000000000, 37.00000000000002132 ) ) ;
#287=ORIENTED_EDGE ( 'NONE', *, *, #15417, .F. ) ;
#300=EDGE_CURVE ( 'NONE', #18143, #9184, #13721, .T. ) ;
#302=CARTESIAN_POINT ( 'NONE',  ( 31.00000000000002842, 0.000000000000000000, 23.00000000000001066 ) ) ;
#354=CARTESIAN_POINT ( 'NONE',  ( 37.00000000000000000, 68.00000000000000000, -23.00000000000000000 ) ) ;
#380=DIRECTION ( 'NONE',  ( 1.000000000000000000, -0.000000000000000000, 0.000000000000000000 ) ) ;
#381=LINE ( 'NONE', #7755, #630 ) ;
#397=CARTESIAN_POINT ( 'NONE',  ( -25.99999999999999645, 68.00000000000000000, -31.00000000000003197 ) ) ;
#404=FACE_OUTER_BOUND ( 'NONE', #1206, .T. ) ;
#430=DIRECTION ( 'NONE',  ( -0.000000000000000000, -0.000000000000000000, 1.000000000000000000 ) ) ;
#451=VECTOR ( 'NONE', #11887, 1000.000000000000000 ) ;
#453=PLANE ( 'NONE',  #12031 ) ;
#503=VERTEX_POINT ( 'NONE', #13112 ) ;
#524=ADVANCED_BREP_SHAPE_REPRESENTATION ( '', ( #1644, #2741 ), #6708 ) ;
#528=ORIENTED_EDGE ( 'NONE', *, *, #9807, .F. ) ;
#560=ADVANCED_FACE ( 'NONE', ( #14938 ), #5654, .F. ) ;
#561=EDGE_CURVE ( 'NONE', #9020, #14418, #12236, .T. ) ;
#575=ORIENTED_EDGE ( 'NONE', *, *, #4462, .T. ) ;
#586=CARTESIAN_POINT ( 'NONE',  ( 37.00000000000000000, 68.00000000000000000, -23.00000000000000000 ) ) ;
#630=VECTOR ( 'NONE', #3391, 1000.000000000000000 ) ;
#653=AXIS2_PLACEMENT_3D ( 'NONE', #4126, #7308, #10403 ) ;
#666=VERTEX_POINT ( 'NONE', #19853 ) ;
#673=LINE ( 'NONE', #19332, #17014 ) ;
#685=FACE_OUTER_BOUND ( 'NONE', #7571, .T. ) ;
#703=LINE ( 'NONE', #19653, #11446 ) ;
#720=VECTOR ( 'NONE', #2438, 1000.000000000000000 ) ;
#735=AXIS2_PLACEMENT_3D ( 'NONE', #5851, #16780, #4505 ) ;
#739=EDGE_LOOP ( 'NONE', ( #2675, #7666, #18295, #18706 ) ) ;
#799=ORIENTED_EDGE ( 'NONE', *, *, #19683, .T. ) ;
#871=CARTESIAN_POINT ( 'NONE',  ( 23.00000000000000711, 68.00000000000000000, -31.00000000000002487 ) ) ;
#913=DIRECTION ( 'NONE',  ( -1.000000000000000000, -0.000000000000000000, 1.156482317317883755E-15 ) ) ;
#933=ORIENTED_EDGE ( 'NONE', *, *, #19168, .F. ) ;
#935=CYLINDRICAL_SURFACE ( 'NONE', #8557, 4.999999999999997335 ) ;
#943=CARTESIAN_POINT ( 'NONE',  ( -40.00000000000000000, 68.00000000000000000, 26.00000000000000355 ) ) ;
#944=EDGE_LOOP ( 'NONE', ( #19895, #6030, #14541, #6367, #11037, #14112, #4467, #2193, #1727, #10650, #9732, #9960, #16124, #7904, #18485, #9733 ) ) ;
#998=EDGE_LOOP ( 'NONE', ( #3956, #2228, #1884, #18628, #12737, #11202, #1629, #3238, #17351, #5028, #16860, #14048, #15733, #15344, #1597, #11329 ) ) ;
#1011=VECTOR ( 'NONE', #15229, 1000.000000000000000 ) ;
#1042=PLANE ( 'NONE',  #111 ) ;
#1054=EDGE_LOOP ( 'NONE', ( #19573, #8675, #19299, #7566 ) ) ;
#1055=CARTESIAN_POINT ( 'NONE',  ( -31.00000000000003197, 0.000000000000000000, 26.00000000000000355 ) ) ;
#1087=CARTESIAN_POINT ( 'NONE',  ( 40.00000000000000000, 68.00000000000000000, -25.99999999999999645 ) ) ;
#1135=ORIENTED_EDGE ( 'NONE', *, *, #19807, .F. ) ;
#1144=EDGE_CURVE ( 'NONE', #19923, #666, #17154, .T. ) ;
#1166=AXIS2_PLACEMENT_3D ( 'NONE', #18221, #7216, #2239 ) ;
#1170=PLANE ( 'NONE',  #735 ) ;
#1198=ADVANCED_FACE ( 'NONE', ( #19104 ), #453, .T. ) ;
#1201=( NAMED_UNIT ( * ) SI_UNIT ( $, .STERADIAN. ) SOLID_ANGLE_UNIT ( ) );
#1206=EDGE_LOOP ( 'NONE', ( #17914, #14852, #575, #8505 ) ) ;
#1207=CARTESIAN_POINT ( 'NONE',  ( -22.99999999999999645, 68.00000000000000000, -36.99999999999999289 ) ) ;
#1212=CYLINDRICAL_SURFACE ( 'NONE', #20170, 5.000000000000000888 ) ;
#1232=CARTESIAN_POINT ( 'NONE',  ( 31.00000000000002842, 68.00000000000000000, 26.00000000000001066 ) ) ;
#1272=ORIENTED_EDGE ( 'NONE', *, *, #5335, .F. ) ;
#1301=ORIENTED_EDGE ( 'NONE', *, *, #16523, .F. ) ;
#1344=VECTOR ( 'NONE', #19201, 1000.000000000000000 ) ;
#1345=ORIENTED_EDGE ( 'NONE', *, *, #3338, .T. ) ;
#1359=DIRECTION ( 'NONE',  ( 1.000000000000000000, 0.000000000000000000, 0.000000000000000000 ) ) ;
#1455=EDGE_CURVE ( 'NONE', #19399, #19379, #4978, .T. ) ;
#1474=VECTOR ( 'NONE', #12030, 1000.000000000000000 ) ;
#1478=CARTESIAN_POINT ( 'NONE',  ( -25.99999999999999645, 68.00000000000000000, -39.99999999999999289 ) ) ;
#1484=FACE_OUTER_BOUND ( 'NONE', #19692, .T. ) ;
#1505=ORIENTED_EDGE ( 'NONE', *, *, #18314, .T. ) ;
#1513=EDGE_CURVE ( 'NONE', #11555, #7705, #18227, .T. ) ;
#1525=CARTESIAN_POINT ( 'NONE',  ( 30.99999999999999645, 68.00000000000000000, 31.00000000000001066 ) ) ;
#1530=CARTESIAN_POINT ( 'NONE',  ( 31.00000000000006395, 0.000000000000000000, -22.99999999999999289 ) ) ;
#1584=AXIS2_PLACEMENT_3D ( 'NONE', #18046, #2182, #16136 ) ;
#1597=ORIENTED_EDGE ( 'NONE', *, *, #1144, .F. ) ;
#1609=AXIS2_PLACEMENT_3D ( 'NONE', #6249, #9025, #12119 ) ;
#1629=ORIENTED_EDGE ( 'NONE', *, *, #9788, .F. ) ;
#1644=MANIFOLD_SOLID_BREP ( 'Boss-Extrude1', #7677 ) ;
#1664=EDGE_CURVE ( 'NONE', #4662, #19129, #4435, .T. ) ;
#1667=CARTESIAN_POINT ( 'NONE',  ( -37.00000000000000000, 68.00000000000000000, 23.00000000000000355 ) ) ;
#1693=ORIENTED_EDGE ( 'NONE', *, *, #19168, .T. ) ;
#1696=VERTEX_POINT ( 'NONE', #4744 ) ;
#1727=ORIENTED_EDGE ( 'NONE', *, *, #14220, .T. ) ;
#1759=VECTOR ( 'NONE', #3856, 1000.000000000000000 ) ;
#1770=CARTESIAN_POINT ( 'NONE',  ( -40.00000000000000000, 0.000000000000000000, -25.99999999999999645 ) ) ;
#1795=CARTESIAN_POINT ( 'NONE',  ( -31.00000000000003197, 68.00000000000000000, 26.00000000000000355 ) ) ;
#1817=EDGE_CURVE ( 'NONE', #666, #3145, #12693, .T. ) ;
#1841=ORIENTED_EDGE ( 'NONE', *, *, #3464, .F. ) ;
#1866=CARTESIAN_POINT ( 'NONE',  ( 25.99999999999999645, 68.00000000000000000, 31.00000000000004619 ) ) ;
#1867=DIRECTION ( 'NONE',  ( 0.000000000000000000, 0.000000000000000000, -1.000000000000000000 ) ) ;
#1884=ORIENTED_EDGE ( 'NONE', *, *, #17957, .F. ) ;
#1885=DIRECTION ( 'NONE',  ( 0.000000000000000000, 0.000000000000000000, 1.000000000000000000 ) ) ;
#1904=CARTESIAN_POINT ( 'NONE',  ( -23.00000000000000000, 68.00000000000000000, -31.00000000000005684 ) ) ;
#1910=DIRECTION ( 'NONE',  ( -1.000000000000000000, -0.000000000000000000, -0.000000000000000000 ) ) ;
#1915=DIRECTION ( 'NONE',  ( -0.000000000000000000, -1.000000000000000000, 0.000000000000000000 ) ) ;
#1934=CARTESIAN_POINT ( 'NONE',  ( 25.99999999999999645, 0.000000000000000000, -39.99999999999999289 ) ) ;
#1939=AXIS2_PLACEMENT_3D ( 'NONE', #16590, #11840, #13489 ) ;
#1962=DIRECTION ( 'NONE',  ( -0.000000000000000000, -1.000000000000000000, -0.000000000000000000 ) ) ;
#1990=LINE ( 'NONE', #19317, #19238 ) ;
#2001=VERTEX_POINT ( 'NONE', #1055 ) ;
#2008=ORIENTED_EDGE ( 'NONE', *, *, #19260, .F. ) ;
#2009=CARTESIAN_POINT ( 'NONE',  ( 31.00000000000002842, 68.00000000000000000, 23.00000000000001066 ) ) ;
#2037=PLANE ( 'NONE',  #19550 ) ;
#2046=EDGE_CURVE ( 'NONE', #18003, #503, #12760, .T. ) ;
#2056=EDGE_LOOP ( 'NONE', ( #10422, #7508, #11914, #799 ) ) ;
#2067=CARTESIAN_POINT ( 'NONE',  ( -31.00000000000002842, 68.00000000000000000, -25.99999999999999645 ) ) ;
#2070=ORIENTED_EDGE ( 'NONE', *, *, #1455, .T. ) ;
#2080=VECTOR ( 'NONE', #12265, 1000.000000000000000 ) ;
#2084=CIRCLE ( 'NONE', #12999, 8.000000000000000000 ) ;
#2108=DIRECTION ( 'NONE',  ( -0.000000000000000000, -0.000000000000000000, 1.000000000000000000 ) ) ;
#2109=EDGE_CURVE ( 'NONE', #9451, #9045, #9108, .T. ) ;
#2117=EDGE_LOOP ( 'NONE', ( #7011, #20203, #11383, #9350, #2366, #4082, #11985, #287, #933, #14652, #16890, #8101, #15522, #12348, #1272, #5792 ) ) ;
#2119=CARTESIAN_POINT ( 'NONE',  ( 31.00000000000000711, 0.000000000000000000, -30.99999999999999289 ) ) ;
#2120=VECTOR ( 'NONE', #11148, 1000.000000000000000 ) ;
#2182=DIRECTION ( 'NONE',  ( -0.000000000000000000, -1.000000000000000000, 0.000000000000000000 ) ) ;
#2193=ORIENTED_EDGE ( 'NONE', *, *, #13762, .T. ) ;
#2200=VECTOR ( 'NONE', #19756, 1000.000000000000000 ) ;
#2212=ORIENTED_EDGE ( 'NONE', *, *, #3838, .F. ) ;
#2224=LINE ( 'NONE', #8523, #20220 ) ;
#2228=ORIENTED_EDGE ( 'NONE', *, *, #9900, .F. ) ;
#2239=DIRECTION ( 'NONE',  ( 0.000000000000000000, 0.000000000000000000, -1.000000000000000000 ) ) ;
#2255=ORIENTED_EDGE ( 'NONE', *, *, #9807, .T. ) ;
#2271=LINE ( 'NONE', #2500, #6735 ) ;
#2298=ORIENTED_EDGE ( 'NONE', *, *, #2803, .T. ) ;
#2316=DIRECTION ( 'NONE',  ( 0.000000000000000000, 0.000000000000000000, -1.000000000000000000 ) ) ;
#2342=EDGE_CURVE ( 'NONE', #7513, #9045, #14549, .T. ) ;
#2346=FACE_OUTER_BOUND ( 'NONE', #4948, .T. ) ;
#2366=ORIENTED_EDGE ( 'NONE', *, *, #2803, .F. ) ;
#2379=CARTESIAN_POINT ( 'NONE',  ( -25.99999999999999645, 0.000000000000000000, -39.99999999999999289 ) ) ;
#2388=VECTOR ( 'NONE', #13121, 1000.000000000000000 ) ;
#2389=ORIENTED_EDGE ( 'NONE', *, *, #14416, .T. ) ;
#2391=EDGE_CURVE ( 'NONE', #2478, #2627, #15067, .T. ) ;
#2426=VECTOR ( 'NONE', #6943, 1000.000000000000000 ) ;
#2438=DIRECTION ( 'NONE',  ( -0.000000000000000000, -1.000000000000000000, -0.000000000000000000 ) ) ;
#2459=DIRECTION ( 'NONE',  ( 0.000000000000000000, 0.000000000000000000, -1.000000000000000000 ) ) ;
#2469=DIRECTION ( 'NONE',  ( 0.000000000000000000, 0.000000000000000000, -1.000000000000000000 ) ) ;
#2478=VERTEX_POINT ( 'NONE', #8786 ) ;
#2500=CARTESIAN_POINT ( 'NONE',  ( 31.00000000000002842, 68.00000000000000000, 23.00000000000001066 ) ) ;
#2538=CARTESIAN_POINT ( 'NONE',  ( -22.99999999999999645, 68.00000000000000000, -31.00000000000005684 ) ) ;
#2547=ORIENTED_EDGE ( 'NONE', *, *, #2046, .T. ) ;
#2552=CARTESIAN_POINT ( 'NONE',  ( 31.00000000000000711, 68.00000000000000000, -30.99999999999999289 ) ) ;
#2569=ORIENTED_EDGE ( 'NONE', *, *, #18097, .T. ) ;
#2599=VERTEX_POINT ( 'NONE', #13009 ) ;
#2611=FACE_OUTER_BOUND ( 'NONE', #12353, .T. ) ;
#2627=VERTEX_POINT ( 'NONE', #1934 ) ;
#2630=EDGE_CURVE ( 'NONE', #13356, #14748, #17638, .T. ) ;
#2675=ORIENTED_EDGE ( 'NONE', *, *, #17306, .T. ) ;
#2682=FILL_AREA_STYLE_COLOUR ( '', #8047 ) ;
#2722=EDGE_CURVE ( 'NONE', #13882, #19875, #16032, .T. ) ;
#2730=VECTOR ( 'NONE', #1359, 1000.000000000000000 ) ;
#2741=AXIS2_PLACEMENT_3D ( 'NONE', #5042, #3500, #8234 ) ;
#2770=CARTESIAN_POINT ( 'NONE',  ( -37.00000000000000000, 68.00000000000000000, -22.99999999999999645 ) ) ;
#2788=( LENGTH_UNIT ( ) NAMED_UNIT ( * ) SI_UNIT ( .MILLI., .METRE. ) );
#2803=EDGE_CURVE ( 'NONE', #3148, #11681, #9997, .T. ) ;
#2966=VECTOR ( 'NONE', #8079, 1000.000000000000000 ) ;
#2969=CARTESIAN_POINT ( 'NONE',  ( 37.00000000000000000, 68.00000000000000000, 23.00000000000001066 ) ) ;
#2978=ORIENTED_EDGE ( 'NONE', *, *, #14416, .F. ) ;
#2981=AXIS2_PLACEMENT_3D ( 'NONE', #10858, #15623, #15516 ) ;
#2985=LINE ( 'NONE', #10428, #10912 ) ;
#2995=DIRECTION ( 'NONE',  ( 1.000000000000000000, 0.000000000000000000, -0.000000000000000000 ) ) ;
#3030=DIRECTION ( 'NONE',  ( -0.000000000000000000, -0.000000000000000000, 1.000000000000000000 ) ) ;
#3033=VECTOR ( 'NONE', #15958, 1000.000000000000000 ) ;
#3045=VECTOR ( 'NONE', #6458, 1000.000000000000000 ) ;
#3105=ADVANCED_FACE ( 'NONE', ( #5150 ), #11826, .T. ) ;
#3133=LINE ( 'NONE', #12725, #8904 ) ;
#3142=ORIENTED_EDGE ( 'NONE', *, *, #19807, .T. ) ;
#3145=VERTEX_POINT ( 'NONE', #14915 ) ;
#3146=VERTEX_POINT ( 'NONE', #14716 ) ;
#3148=VERTEX_POINT ( 'NONE', #586 ) ;
#3149=VECTOR ( 'NONE', #3539, 1000.000000000000000 ) ;
#3159=EDGE_CURVE ( 'NONE', #9451, #3146, #13183, .T. ) ;
#3168=EDGE_LOOP ( 'NONE', ( #16914, #2978, #2298, #17710 ) ) ;
#3221=CARTESIAN_POINT ( 'NONE',  ( 31.00000000000006395, 68.00000000000000000, -22.99999999999999289 ) ) ;
#3227=DIRECTION ( 'NONE',  ( -0.000000000000000000, -1.000000000000000000, -0.000000000000000000 ) ) ;
#3235=VERTEX_POINT ( 'NONE', #8832 ) ;
#3238=ORIENTED_EDGE ( 'NONE', *, *, #19685, .F. ) ;
#3287=CIRCLE ( 'NONE', #1609, 8.000000000000000000 ) ;
#3332=DIRECTION ( 'NONE',  ( -5.782411586589400040E-16, 0.000000000000000000, 1.000000000000000000 ) ) ;
#3338=EDGE_CURVE ( 'NONE', #2478, #8069, #3353, .T. ) ;
#3353=LINE ( 'NONE', #1478, #3386 ) ;
#3360=DIRECTION ( 'NONE',  ( -1.000000000000000000, -0.000000000000000000, -0.000000000000000000 ) ) ;
#3372=AXIS2_PLACEMENT_3D ( 'NONE', #6696, #1915, #13102 ) ;
#3386=VECTOR ( 'NONE', #4595, 1000.000000000000000 ) ;
#3391=DIRECTION ( 'NONE',  ( -1.000000000000000000, -0.000000000000000000, -0.000000000000000000 ) ) ;
#3393=LINE ( 'NONE', #2969, #15790 ) ;
#3417=EDGE_LOOP ( 'NONE', ( #7184, #8490, #3882, #2569 ) ) ;
#3424=ORIENTED_EDGE ( 'NONE', *, *, #2722, .T. ) ;
#3429=EDGE_CURVE ( 'NONE', #9184, #4662, #5009, .T. ) ;
#3435=AXIS2_PLACEMENT_3D ( 'NONE', #6540, #17438, #3332 ) ;
#3464=EDGE_CURVE ( 'NONE', #8069, #19923, #14692, .T. ) ;
#3465=DIRECTION ( 'NONE',  ( -1.000000000000000000, 0.000000000000000000, 0.000000000000000000 ) ) ;
#3500=DIRECTION ( 'NONE',  ( 0.000000000000000000, 0.000000000000000000, 1.000000000000000000 ) ) ;
#3502=CARTESIAN_POINT ( 'NONE',  ( 26.00000000000000711, 68.00000000000000000, -31.00000000000002487 ) ) ;
#3503=DIRECTION ( 'NONE',  ( 1.000000000000000000, 0.000000000000000000, 0.000000000000000000 ) ) ;
#3507=VERTEX_POINT ( 'NONE', #1530 ) ;
#3539=DIRECTION ( 'NONE',  ( -0.000000000000000000, -0.000000000000000000, 1.000000000000000000 ) ) ;
#3547=CARTESIAN_POINT ( 'NONE',  ( 22.99999999999999289, 68.00000000000000000, 37.00000000000002132 ) ) ;
#3552=APPLICATION_CONTEXT ( 'automotive_design' ) ;
#3555=ORIENTED_EDGE ( 'NONE', *, *, #3464, .T. ) ;
#3559=CIRCLE ( 'NONE', #19647, 4.999999999999997335 ) ;
#3570=ORIENTED_EDGE ( 'NONE', *, *, #1513, .F. ) ;
#3578=ORIENTED_EDGE ( 'NONE', *, *, #9762, .T. ) ;
#3581=VERTEX_POINT ( 'NONE', #13921 ) ;
#3597=SHAPE_REPRESENTATION_RELATIONSHIP ( 'NONE' , 'NONE' ,  #8923, #524 ) ;
#3600=PLANE ( 'NONE',  #14223 ) ;
#3635=EDGE_LOOP ( 'NONE', ( #15087, #9200, #2212, #9055 ) ) ;
#3647=LINE ( 'NONE', #3547, #1759 ) ;
#3648=VECTOR ( 'NONE', #10811, 1000.000000000000000 ) ;
#3650=VECTOR ( 'NONE', #1962, 1000.000000000000000 ) ;
#3678=CARTESIAN_POINT ( 'NONE',  ( 30.99999999999999645, 0.000000000000000000, 31.00000000000001066 ) ) ;
#3691=AXIS2_PLACEMENT_3D ( 'NONE', #3678, #8323, #17788 ) ;
#3693=( NAMED_UNIT ( * ) PLANE_ANGLE_UNIT ( ) SI_UNIT ( $, .RADIAN. ) );
#3702=PRODUCT_DEFINITION_CONTEXT ( 'detailed design', #3552, 'design' ) ;
#3723=CIRCLE ( 'NONE', #17860, 8.000000000000000000 ) ;
#3741=DIRECTION ( 'NONE',  ( -0.000000000000000000, -1.000000000000000000, -0.000000000000000000 ) ) ;
#3742=VECTOR ( 'NONE', #16904, 1000.000000000000000 ) ;
#3747=DIRECTION ( 'NONE',  ( 0.000000000000000000, 0.000000000000000000, -1.000000000000000000 ) ) ;
#3750=EDGE_LOOP ( 'NONE', ( #17447, #18910, #9268, #18739 ) ) ;
#3788=CARTESIAN_POINT ( 'NONE',  ( 40.00000000000000000, 0.000000000000000000, 26.00000000000000355 ) ) ;
#3817=VECTOR ( 'NONE', #5681, 1000.000000000000000 ) ;
#3838=EDGE_CURVE ( 'NONE', #18751, #9451, #6926, .T. ) ;
#3844=CARTESIAN_POINT ( 'NONE',  ( 31.00000000000004263, 68.00000000000000000, -25.99999999999999645 ) ) ;
#3847=VECTOR ( 'NONE', #8612, 1000.000000000000000 ) ;
#3856=DIRECTION ( 'NONE',  ( 5.782411586589399054E-16, 0.000000000000000000, -1.000000000000000000 ) ) ;
#3882=ORIENTED_EDGE ( 'NONE', *, *, #4995, .T. ) ;
#3897=DIRECTION ( 'NONE',  ( 0.000000000000000000, 0.000000000000000000, -1.000000000000000000 ) ) ;
#3941=CARTESIAN_POINT ( 'NONE',  ( -25.99999999999999645, 0.000000000000000000, -39.99999999999999289 ) ) ;
#3948=EDGE_CURVE ( 'NONE', #11627, #7970, #703, .T. ) ;
#3953=ORIENTED_EDGE ( 'NONE', *, *, #18444, .F. ) ;
#3955=DIRECTION ( 'NONE',  ( 1.000000000000000000, 0.000000000000000000, -7.709882115452498874E-16 ) ) ;
#3956=ORIENTED_EDGE ( 'NONE', *, *, #7600, .F. ) ;
#3981=LINE ( 'NONE', #3788, #9429 ) ;
#3985=DIRECTION ( 'NONE',  ( 0.000000000000000000, 0.000000000000000000, -1.000000000000000000 ) ) ;
#4008=AXIS2_PLACEMENT_3D ( 'NONE', #8512, #14797, #17992 ) ;
#4011=CARTESIAN_POINT ( 'NONE',  ( -22.99999999999999645, 0.000000000000000000, 37.00000000000002132 ) ) ;
#4018=LINE ( 'NONE', #5375, #12005 ) ;
#4049=LINE ( 'NONE', #5589, #451 ) ;
#4075=FACE_OUTER_BOUND ( 'NONE', #18435, .T. ) ;
#4082=ORIENTED_EDGE ( 'NONE', *, *, #16098, .F. ) ;
#4086=VECTOR ( 'NONE', #16898, 1000.000000000000000 ) ;
#4119=ORIENTED_EDGE ( 'NONE', *, *, #11953, .T. ) ;
#4125=CARTESIAN_POINT ( 'NONE',  ( -37.00000000000000000, 68.00000000000000000, 23.00000000000000355 ) ) ;
#4126=CARTESIAN_POINT ( 'NONE',  ( 25.99999999999999645, 68.00000000000000000, 40.00000000000002132 ) ) ;
#4176=DIRECTION ( 'NONE',  ( 0.000000000000000000, 0.000000000000000000, -1.000000000000000000 ) ) ;
#4257=ORIENTED_EDGE ( 'NONE', *, *, #18795, .F. ) ;
#4270=CARTESIAN_POINT ( 'NONE',  ( -31.00000000000002842, 68.00000000000000000, -25.99999999999999645 ) ) ;
#4381=EDGE_LOOP ( 'NONE', ( #17015, #2008, #6143, #14107 ) ) ;
#4393=LINE ( 'NONE', #10272, #720 ) ;
#4435=LINE ( 'NONE', #9380, #133 ) ;
#4449=VECTOR ( 'NONE', #11783, 1000.000000000000000 ) ;
#4455=DIRECTION ( 'NONE',  ( 0.000000000000000000, 0.000000000000000000, -1.000000000000000000 ) ) ;
#4462=EDGE_CURVE ( 'NONE', #9184, #9751, #13769, .T. ) ;
#4467=ORIENTED_EDGE ( 'NONE', *, *, #6541, .T. ) ;
#4488=ORIENTED_EDGE ( 'NONE', *, *, #16002, .T. ) ;
#4497=PLANE ( 'NONE',  #8330 ) ;
#4505=DIRECTION ( 'NONE',  ( -1.000000000000000000, 0.000000000000000000, 7.709882115452498874E-16 ) ) ;
#4529=CARTESIAN_POINT ( 'NONE',  ( -40.00000000000000000, 0.000000000000000000, -25.99999999999999645 ) ) ;
#4541=EDGE_LOOP ( 'NONE', ( #6003, #7380, #10718, #19268 ) ) ;
#4550=CARTESIAN_POINT ( 'NONE',  ( 22.99999999999999645, 0.000000000000000000, 31.00000000000006750 ) ) ;
#4556=CARTESIAN_POINT ( 'NONE',  ( 31.00000000000004263, 0.000000000000000000, -25.99999999999999645 ) ) ;
#4561=EDGE_CURVE ( 'NONE', #18003, #12618, #10885, .T. ) ;
#4574=PLANE ( 'NONE',  #2981 ) ;
#4595=DIRECTION ( 'NONE',  ( -1.000000000000000000, -0.000000000000000000, -0.000000000000000000 ) ) ;
#4616=VERTEX_POINT ( 'NONE', #6259 ) ;
#4621=DIRECTION ( 'NONE',  ( -0.000000000000000000, -1.000000000000000000, 0.000000000000000000 ) ) ;
#4632=CARTESIAN_POINT ( 'NONE',  ( -40.00000000000000000, 68.00000000000000000, -25.99999999999999645 ) ) ;
#4662=VERTEX_POINT ( 'NONE', #5014 ) ;
#4669=DIRECTION ( 'NONE',  ( -0.000000000000000000, -1.000000000000000000, -0.000000000000000000 ) ) ;
#4718=CARTESIAN_POINT ( 'NONE',  ( -25.99999999999999645, 68.00000000000000000, -39.99999999999999289 ) ) ;
#4744=CARTESIAN_POINT ( 'NONE',  ( 22.99999999999999289, 68.00000000000000000, 37.00000000000002132 ) ) ;
#4745=EDGE_LOOP ( 'NONE', ( #10570, #528, #17907, #4488 ) ) ;
#4752=ORIENTED_EDGE ( 'NONE', *, *, #1144, .T. ) ;
#4808=DIRECTION ( 'NONE',  ( 1.000000000000000000, 0.000000000000000000, -0.000000000000000000 ) ) ;
#4815=LINE ( 'NONE', #20258, #9610 ) ;
#4842=CARTESIAN_POINT ( 'NONE',  ( -25.99999999999999645, 68.00000000000000000, -39.99999999999999289 ) ) ;
#4850=ORIENTED_EDGE ( 'NONE', *, *, #15326, .T. ) ;
#4886=SHAPE_DEFINITION_REPRESENTATION ( #9420, #8923 ) ;
#4894=VERTEX_POINT ( 'NONE', #15923 ) ;
#4907=DIRECTION ( 'NONE',  ( 0.000000000000000000, 0.000000000000000000, -1.000000000000000000 ) ) ;
#4917=CARTESIAN_POINT ( 'NONE',  ( -22.99999999999999645, 68.00000000000000000, 31.00000000000003908 ) ) ;
#4948=EDGE_LOOP ( 'NONE', ( #5406, #17429, #5904, #2547 ) ) ;
#4950=LINE ( 'NONE', #17210, #7056 ) ;
#4954=AXIS2_PLACEMENT_3D ( 'NONE', #16707, #17920, #13205 ) ;
#4960=CARTESIAN_POINT ( 'NONE',  ( 37.00000000000000000, 68.00000000000000000, 23.00000000000001066 ) ) ;
#4962=ORIENTED_EDGE ( 'NONE', *, *, #5893, .T. ) ;
#4978=LINE ( 'NONE', #3844, #2426 ) ;
#4988=DIRECTION ( 'NONE',  ( -0.000000000000000000, -0.000000000000000000, 1.000000000000000000 ) ) ;
#4995=EDGE_CURVE ( 'NONE', #17171, #9020, #14362, .T. ) ;
#5009=LINE ( 'NONE', #154, #3045 ) ;
#5014=CARTESIAN_POINT ( 'NONE',  ( -23.00000000000000000, 0.000000000000000000, -36.99999999999999289 ) ) ;
#5028=ORIENTED_EDGE ( 'NONE', *, *, #17306, .F. ) ;
#5037=DIRECTION ( 'NONE',  ( 0.000000000000000000, 0.000000000000000000, -1.000000000000000000 ) ) ;
#5042=CARTESIAN_POINT ( 'NONE',  ( 0.000000000000000000, 0.000000000000000000, 0.000000000000000000 ) ) ;
#5067=EDGE_CURVE ( 'NONE', #14445, #18751, #10490, .T. ) ;
#5150=FACE_OUTER_BOUND ( 'NONE', #12766, .T. ) ;
#5157=( NAMED_UNIT ( * ) SI_UNIT ( $, .STERADIAN. ) SOLID_ANGLE_UNIT ( ) );
#5177=CARTESIAN_POINT ( 'NONE',  ( -22.99999999999999645, 68.00000000000000000, -31.00000000000005684 ) ) ;
#5178=PLANE ( 'NONE',  #8909 ) ;
#5184=CARTESIAN_POINT ( 'NONE',  ( -30.99999999999999645, 0.000000000000000000, -30.99999999999999289 ) ) ;
#5187=FACE_BOUND ( 'NONE', #944, .T. ) ;
#5195=ADVANCED_FACE ( 'NONE', ( #20204 ), #5248, .F. ) ;
#5248=PLANE ( 'NONE',  #15793 ) ;
#5258=ORIENTED_EDGE ( 'NONE', *, *, #15417, .T. ) ;
#5335=EDGE_CURVE ( 'NONE', #17102, #17171, #381, .T. ) ;
#5350=ORIENTED_EDGE ( 'NONE', *, *, #14596, .F. ) ;
#5370=AXIS2_PLACEMENT_3D ( 'NONE', #7802, #4907, #6464 ) ;
#5375=CARTESIAN_POINT ( 'NONE',  ( 23.00000000000000711, 68.00000000000000000, -36.99999999999999289 ) ) ;
#5393=LINE ( 'NONE', #16132, #7019 ) ;
#5406=ORIENTED_EDGE ( 'NONE', *, *, #6541, .F. ) ;
#5439=VECTOR ( 'NONE', #1910, 1000.000000000000000 ) ;
#5445=AXIS2_PLACEMENT_3D ( 'NONE', #10297, #10676, #8541 ) ;
#5454=DIRECTION ( 'NONE',  ( -0.000000000000000000, -1.000000000000000000, -0.000000000000000000 ) ) ;
#5484=EDGE_CURVE ( 'NONE', #7013, #3581, #12049, .T. ) ;
#5492=DIRECTION ( 'NONE',  ( -0.000000000000000000, -1.000000000000000000, -0.000000000000000000 ) ) ;
#5504=ORIENTED_EDGE ( 'NONE', *, *, #11420, .F. ) ;
#5583=DIRECTION ( 'NONE',  ( 0.000000000000000000, 0.000000000000000000, -1.000000000000000000 ) ) ;
#5584=DIRECTION ( 'NONE',  ( -0.000000000000000000, -1.000000000000000000, -0.000000000000000000 ) ) ;
#5589=CARTESIAN_POINT ( 'NONE',  ( -40.00000000000000000, 68.00000000000000000, -25.99999999999999645 ) ) ;
#5654=CYLINDRICAL_SURFACE ( 'NONE', #11002, 4.999999999999997335 ) ;
#5678=CIRCLE ( 'NONE', #3372, 8.000000000000000000 ) ;
#5681=DIRECTION ( 'NONE',  ( -0.000000000000000000, -1.000000000000000000, -0.000000000000000000 ) ) ;
#5702=FACE_OUTER_BOUND ( 'NONE', #4541, .T. ) ;
#5772=CARTESIAN_POINT ( 'NONE',  ( -25.99999999999999645, 68.00000000000000000, 40.00000000000002132 ) ) ;
#5792=ORIENTED_EDGE ( 'NONE', *, *, #13370, .F. ) ;
#5803=DIRECTION ( 'NONE',  ( -0.000000000000000000, -1.000000000000000000, -0.000000000000000000 ) ) ;
#5836=ORIENTED_EDGE ( 'NONE', *, *, #10758, .F. ) ;
#5851=CARTESIAN_POINT ( 'NONE',  ( 31.00000000000002842, 68.00000000000000000, 26.00000000000001066 ) ) ;
#5860=ADVANCED_FACE ( 'NONE', ( #5909 ), #935, .F. ) ;
#5867=ADVANCED_FACE ( 'NONE', ( #15394 ), #19691, .T. ) ;
#5893=EDGE_CURVE ( 'NONE', #8326, #9383, #16656, .T. ) ;
#5904=ORIENTED_EDGE ( 'NONE', *, *, #15710, .T. ) ;
#5906=AXIS2_PLACEMENT_3D ( 'NONE', #12145, #4621, #20056 ) ;
#5909=FACE_OUTER_BOUND ( 'NONE', #739, .T. ) ;
#5939=CARTESIAN_POINT ( 'NONE',  ( 25.99999999999999645, 0.000000000000000000, 40.00000000000002132 ) ) ;
#5957=DIRECTION ( 'NONE',  ( 1.000000000000000000, 0.000000000000000000, 0.000000000000000000 ) ) ;
#5973=EDGE_CURVE ( 'NONE', #11681, #3507, #20, .T. ) ;
#6003=ORIENTED_EDGE ( 'NONE', *, *, #10043, .F. ) ;
#6019=DIRECTION ( 'NONE',  ( -0.000000000000000000, -1.000000000000000000, -0.000000000000000000 ) ) ;
#6030=ORIENTED_EDGE ( 'NONE', *, *, #1664, .T. ) ;
#6058=VERTEX_POINT ( 'NONE', #14444 ) ;
#6108=AXIS2_PLACEMENT_3D ( 'NONE', #8744, #12223, #3897 ) ;
#6116=FACE_OUTER_BOUND ( 'NONE', #4381, .T. ) ;
#6143=ORIENTED_EDGE ( 'NONE', *, *, #11953, .F. ) ;
#6150=AXIS2_PLACEMENT_3D ( 'NONE', #10487, #8938, #15239 ) ;
#6159=FACE_OUTER_BOUND ( 'NONE', #3417, .T. ) ;
#6195=EDGE_LOOP ( 'NONE', ( #5836, #11775, #7732, #13663 ) ) ;
#6210=CARTESIAN_POINT ( 'NONE',  ( 31.00000000000006395, 68.00000000000000000, -22.99999999999999289 ) ) ;
#6246=ORIENTED_EDGE ( 'NONE', *, *, #17446, .T. ) ;
#6249=CARTESIAN_POINT ( 'NONE',  ( 31.00000000000000711, 0.000000000000000000, -30.99999999999999289 ) ) ;
#6259=CARTESIAN_POINT ( 'NONE',  ( 26.00000000000001066, 68.00000000000000000, -31.00000000000002487 ) ) ;
#6261=LINE ( 'NONE', #6565, #9664 ) ;
#6292=VECTOR ( 'NONE', #18226, 1000.000000000000000 ) ;
#6320=VECTOR ( 'NONE', #2108, 1000.000000000000000 ) ;
#6335=ORIENTED_EDGE ( 'NONE', *, *, #5973, .F. ) ;
#6345=ORIENTED_EDGE ( 'NONE', *, *, #561, .T. ) ;
#6360=DIRECTION ( 'NONE',  ( 1.000000000000000000, 0.000000000000000000, -0.000000000000000000 ) ) ;
#6367=ORIENTED_EDGE ( 'NONE', *, *, #6448, .T. ) ;
#6442=FACE_OUTER_BOUND ( 'NONE', #8908, .T. ) ;
#6448=EDGE_CURVE ( 'NONE', #2599, #7013, #14828, .T. ) ;
#6458=DIRECTION ( 'NONE',  ( -0.000000000000000000, -1.000000000000000000, -0.000000000000000000 ) ) ;
#6464=DIRECTION ( 'NONE',  ( -1.000000000000000000, 0.000000000000000000, -0.000000000000000000 ) ) ;
#6467=AXIS2_PLACEMENT_3D ( 'NONE', #1525, #9574, #9688 ) ;
#6478=ORIENTED_EDGE ( 'NONE', *, *, #16523, .T. ) ;
#6539=DIRECTION ( 'NONE',  ( 5.782411586589399054E-16, 0.000000000000000000, -1.000000000000000000 ) ) ;
#6540=CARTESIAN_POINT ( 'NONE',  ( 22.99999999999999289, 68.00000000000000000, 37.00000000000002132 ) ) ;
#6541=EDGE_CURVE ( 'NONE', #11558, #503, #14787, .T. ) ;
#6548=VECTOR ( 'NONE', #4988, 1000.000000000000000 ) ;
#6565=CARTESIAN_POINT ( 'NONE',  ( 31.00000000000002842, 0.000000000000000000, 23.00000000000001066 ) ) ;
#6603=ORIENTED_EDGE ( 'NONE', *, *, #12551, .F. ) ;
#6620=ADVANCED_FACE ( 'NONE', ( #19018 ), #14606, .T. ) ;
#6636=CARTESIAN_POINT ( 'NONE',  ( -25.99999999999999645, 68.00000000000000000, -31.00000000000003197 ) ) ;
#6639=CARTESIAN_POINT ( 'NONE',  ( 31.00000000000000711, 68.00000000000000000, -30.99999999999999289 ) ) ;
#6696=CARTESIAN_POINT ( 'NONE',  ( -30.99999999999999645, 68.00000000000000000, -30.99999999999999289 ) ) ;
#6697=DIRECTION ( 'NONE',  ( -1.000000000000000000, 0.000000000000000000, 1.156482317317875472E-15 ) ) ;
#6708=( GEOMETRIC_REPRESENTATION_CONTEXT ( 3 ) GLOBAL_UNCERTAINTY_ASSIGNED_CONTEXT ( ( #11943 ) ) GLOBAL_UNIT_ASSIGNED_CONTEXT ( ( #6996, #3693, #5157 ) ) REPRESENTATION_CONTEXT ( 'NONE', 'WORKASPACE' ) );
#6735=VECTOR ( 'NONE', #8797, 1000.000000000000000 ) ;
#6736=DIRECTION ( 'NONE',  ( -0.000000000000000000, -1.000000000000000000, 0.000000000000000000 ) ) ;
#6813=DIRECTION ( 'NONE',  ( 1.156482317317875472E-15, 0.000000000000000000, 1.000000000000000000 ) ) ;
#6814=LINE ( 'NONE', #6907, #16200 ) ;
#6832=LINE ( 'NONE', #4960, #2388 ) ;
#6871=EDGE_CURVE ( 'NONE', #3507, #9496, #3287, .T. ) ;
#6907=CARTESIAN_POINT ( 'NONE',  ( 40.00000000000000000, 68.00000000000000000, 26.00000000000000355 ) ) ;
#6919=CYLINDRICAL_SURFACE ( 'NONE', #4954, 7.999999999999996447 ) ;
#6926=LINE ( 'NONE', #13312, #2200 ) ;
#6943=DIRECTION ( 'NONE',  ( -0.000000000000000000, -1.000000000000000000, -0.000000000000000000 ) ) ;
#6973=ORIENTED_EDGE ( 'NONE', *, *, #19683, .F. ) ;
#6976=VERTEX_POINT ( 'NONE', #11086 ) ;
#6996=( LENGTH_UNIT ( ) NAMED_UNIT ( * ) SI_UNIT ( .MILLI., .METRE. ) );
#7004=ORIENTED_EDGE ( 'NONE', *, *, #6871, .F. ) ;
#7011=ORIENTED_EDGE ( 'NONE', *, *, #4462, .F. ) ;
#7013=VERTEX_POINT ( 'NONE', #19106 ) ;
#7019=VECTOR ( 'NONE', #11570, 1000.000000000000000 ) ;
#7020=LINE ( 'NONE', #4011, #2730 ) ;
#7056=VECTOR ( 'NONE', #14426, 1000.000000000000000 ) ;
#7136=ADVANCED_FACE ( 'NONE', ( #2346 ), #6919, .T. ) ;
#7166=ADVANCED_FACE ( 'NONE', ( #18107 ), #18217, .F. ) ;
#7173=ADVANCED_FACE ( 'NONE', ( #15042 ), #11949, .F. ) ;
#7184=ORIENTED_EDGE ( 'NONE', *, *, #5484, .F. ) ;
#7216=DIRECTION ( 'NONE',  ( -0.000000000000000000, -1.000000000000000000, 0.000000000000000000 ) ) ;
#7223=CARTESIAN_POINT ( 'NONE',  ( -31.00000000000003197, 68.00000000000000000, -22.99999999999999645 ) ) ;
#7234=CARTESIAN_POINT ( 'NONE',  ( -25.99999999999999645, 0.000000000000000000, 31.00000000000003908 ) ) ;
#7239=FILL_AREA_STYLE ('',( #2682 ) ) ;
#7258=DIRECTION ( 'NONE',  ( -0.000000000000000000, -1.000000000000000000, -0.000000000000000000 ) ) ;
#7267=AXIS2_PLACEMENT_3D ( 'NONE', #5772, #8458, #2459 ) ;
#7289=ORIENTED_EDGE ( 'NONE', *, *, #13736, .T. ) ;
#7308=DIRECTION ( 'NONE',  ( -1.000000000000000000, 0.000000000000000000, 0.000000000000000000 ) ) ;
#7357=EDGE_LOOP ( 'NONE', ( #13022, #8293, #14870, #3142 ) ) ;
#7364=DIRECTION ( 'NONE',  ( -0.000000000000000000, -1.000000000000000000, -0.000000000000000000 ) ) ;
#7365=ORIENTED_EDGE ( 'NONE', *, *, #2722, .F. ) ;
#7373=VERTEX_POINT ( 'NONE', #16332 ) ;
#7380=ORIENTED_EDGE ( 'NONE', *, *, #8140, .F. ) ;
#7404=CARTESIAN_POINT ( 'NONE',  ( -37.00000000000000000, 0.000000000000000000, 23.00000000000000355 ) ) ;
#7451=EDGE_CURVE ( 'NONE', #20355, #3507, #11458, .T. ) ;
#7473=CARTESIAN_POINT ( 'NONE',  ( 25.99999999999999645, 0.000000000000000000, 31.00000000000004619 ) ) ;
#7478=CARTESIAN_POINT ( 'NONE',  ( 22.99999999999999289, 0.000000000000000000, 37.00000000000002132 ) ) ;
#7497=ADVANCED_FACE ( 'NONE', ( #8373, #5187 ), #14655, .T. ) ;
#7508=ORIENTED_EDGE ( 'NONE', *, *, #2046, .F. ) ;
#7513=VERTEX_POINT ( 'NONE', #7234 ) ;
#7527=ORIENTED_EDGE ( 'NONE', *, *, #17356, .F. ) ;
#7540=SURFACE_SIDE_STYLE ('',( #15378 ) ) ;
#7562=CARTESIAN_POINT ( 'NONE',  ( -30.99999999999999645, 68.00000000000000000, -30.99999999999999289 ) ) ;
#7563=DIRECTION ( 'NONE',  ( 1.000000000000000000, 0.000000000000000000, -7.709882115452498874E-16 ) ) ;
#7566=ORIENTED_EDGE ( 'NONE', *, *, #11893, .T. ) ;
#7571=EDGE_LOOP ( 'NONE', ( #4752, #9858, #13806, #3555 ) ) ;
#7572=VERTEX_POINT ( 'NONE', #10520 ) ;
#7576=ORIENTED_EDGE ( 'NONE', *, *, #3338, .F. ) ;
#7600=EDGE_CURVE ( 'NONE', #19512, #2627, #2985, .T. ) ;
#7604=ORIENTED_EDGE ( 'NONE', *, *, #1817, .T. ) ;
#7645=CARTESIAN_POINT ( 'NONE',  ( 31.00000000000004263, 68.00000000000000000, -25.99999999999999645 ) ) ;
#7666=ORIENTED_EDGE ( 'NONE', *, *, #8002, .F. ) ;
#7677=CLOSED_SHELL ( 'NONE', ( #11727, #7497, #5195, #13264, #13314, #11143, #19416, #9636, #18190, #5860, #7166, #20086, #7173, #13945, #18489, #18974, #18160, #560, #15070, #10384, #10458, #14292, #5867, #7136, #16279, #3105, #19063, #11508, #6620, #13794, #16836, #8718, #1198, #8269 ) ) ;
#7705=VERTEX_POINT ( 'NONE', #302 ) ;
#7730=ORIENTED_EDGE ( 'NONE', *, *, #9788, .T. ) ;
#7732=ORIENTED_EDGE ( 'NONE', *, *, #300, .T. ) ;
#7755=CARTESIAN_POINT ( 'NONE',  ( -37.00000000000000000, 68.00000000000000000, -22.99999999999999645 ) ) ;
#7764=ORIENTED_EDGE ( 'NONE', *, *, #2630, .T. ) ;
#7789=EDGE_CURVE ( 'NONE', #6058, #11555, #4950, .T. ) ;
#7802=CARTESIAN_POINT ( 'NONE',  ( -40.00000000000000000, 68.00000000000000000, 26.00000000000000355 ) ) ;
#7803=DIRECTION ( 'NONE',  ( -0.000000000000000000, -1.000000000000000000, -0.000000000000000000 ) ) ;
#7814=FACE_OUTER_BOUND ( 'NONE', #3750, .T. ) ;
#7826=DIRECTION ( 'NONE',  ( -0.000000000000000000, -1.000000000000000000, 0.000000000000000000 ) ) ;
#7830=VERTEX_POINT ( 'NONE', #13411 ) ;
#7883=DIRECTION ( 'NONE',  ( 0.000000000000000000, 0.000000000000000000, 1.000000000000000000 ) ) ;
#7896=CARTESIAN_POINT ( 'NONE',  ( -25.99999999999999645, 68.00000000000000000, 31.00000000000003908 ) ) ;
#7904=ORIENTED_EDGE ( 'NONE', *, *, #7451, .T. ) ;
#7905=DIRECTION ( 'NONE',  ( -0.000000000000000000, -1.000000000000000000, -0.000000000000000000 ) ) ;
#7970=VERTEX_POINT ( 'NONE', #1087 ) ;
#7997=CARTESIAN_POINT ( 'NONE',  ( -40.00000000000000000, 68.00000000000000000, -25.99999999999999645 ) ) ;
#8002=EDGE_CURVE ( 'NONE', #18751, #7513, #12238, .T. ) ;
#8040=CARTESIAN_POINT ( 'NONE',  ( -25.99999999999999645, 68.00000000000000000, 40.00000000000002132 ) ) ;
#8047=COLOUR_RGB ( '', 0.66274510, 0.83137255, 0.94901961) ;
#8069=VERTEX_POINT ( 'NONE', #4718 ) ;
#8079=DIRECTION ( 'NONE',  ( -1.000000000000000000, -0.000000000000000000, -0.000000000000000000 ) ) ;
#8101=ORIENTED_EDGE ( 'NONE', *, *, #15710, .F. ) ;
#8114=LINE ( 'NONE', #16066, #14943 ) ;
#8127=ORIENTED_EDGE ( 'NONE', *, *, #13257, .T. ) ;
#8140=EDGE_CURVE ( 'NONE', #9751, #19129, #10075, .T. ) ;
#8189=LINE ( 'NONE', #14363, #9556 ) ;
#8203=CARTESIAN_POINT ( 'NONE',  ( 23.00000000000000711, 68.00000000000000000, -31.00000000000002487 ) ) ;
#8234=DIRECTION ( 'NONE',  ( 1.000000000000000000, 0.000000000000000000, 0.000000000000000000 ) ) ;
#8242=ORIENTED_EDGE ( 'NONE', *, *, #11893, .F. ) ;
#8269=ADVANCED_FACE ( 'NONE', ( #18902 ), #4497, .T. ) ;
#8280=LINE ( 'NONE', #10025, #17859 ) ;
#8293=ORIENTED_EDGE ( 'NONE', *, *, #11174, .F. ) ;
#8319=ORIENTED_EDGE ( 'NONE', *, *, #12411, .F. ) ;
#8323=DIRECTION ( 'NONE',  ( -0.000000000000000000, -1.000000000000000000, 0.000000000000000000 ) ) ;
#8326=VERTEX_POINT ( 'NONE', #12432 ) ;
#8330=AXIS2_PLACEMENT_3D ( 'NONE', #10980, #7883, #4808 ) ;
#8373=FACE_OUTER_BOUND ( 'NONE', #998, .T. ) ;
#8426=EDGE_CURVE ( 'NONE', #11681, #6976, #3723, .T. ) ;
#8435=DIRECTION ( 'NONE',  ( -0.000000000000000000, -1.000000000000000000, 0.000000000000000000 ) ) ;
#8458=DIRECTION ( 'NONE',  ( 1.000000000000000000, -0.000000000000000000, 0.000000000000000000 ) ) ;
#8462=DIRECTION ( 'NONE',  ( -0.000000000000000000, -1.000000000000000000, -0.000000000000000000 ) ) ;
#8490=ORIENTED_EDGE ( 'NONE', *, *, #19952, .F. ) ;
#8497=DIRECTION ( 'NONE',  ( 0.000000000000000000, 0.000000000000000000, -1.000000000000000000 ) ) ;
#8505=ORIENTED_EDGE ( 'NONE', *, *, #8140, .T. ) ;
#8512=CARTESIAN_POINT ( 'NONE',  ( 31.00000000000000711, 68.00000000000000000, -30.99999999999999289 ) ) ;
#8523=CARTESIAN_POINT ( 'NONE',  ( 22.99999999999999289, 68.00000000000000000, 37.00000000000002132 ) ) ;
#8541=DIRECTION ( 'NONE',  ( 0.000000000000000000, 0.000000000000000000, -1.000000000000000000 ) ) ;
#8557=AXIS2_PLACEMENT_3D ( 'NONE', #18153, #7258, #8803 ) ;
#8561=CARTESIAN_POINT ( 'NONE',  ( 25.99999999999999645, 68.00000000000000000, -39.99999999999999289 ) ) ;
#8612=DIRECTION ( 'NONE',  ( -0.000000000000000000, -1.000000000000000000, -0.000000000000000000 ) ) ;
#8618=CARTESIAN_POINT ( 'NONE',  ( -22.99999999999999645, 68.00000000000000000, 37.00000000000002132 ) ) ;
#8620=EDGE_CURVE ( 'NONE', #14600, #8326, #9584, .T. ) ;
#8649=DIRECTION ( 'NONE',  ( -1.000000000000000000, -0.000000000000000000, 1.156482317317883755E-15 ) ) ;
#8672=DIRECTION ( 'NONE',  ( 0.000000000000000000, -1.000000000000000000, 0.000000000000000000 ) ) ;
#8675=ORIENTED_EDGE ( 'NONE', *, *, #1455, .F. ) ;
#8718=ADVANCED_FACE ( 'NONE', ( #11607 ), #10071, .T. ) ;
#8744=CARTESIAN_POINT ( 'NONE',  ( 30.99999999999999645, 68.00000000000000000, 31.00000000000001066 ) ) ;
#8763=DIRECTION ( 'NONE',  ( -1.000000000000000000, -0.000000000000000000, -0.000000000000000000 ) ) ;
#8786=CARTESIAN_POINT ( 'NONE',  ( 25.99999999999999645, 68.00000000000000000, -39.99999999999999289 ) ) ;
#8797=DIRECTION ( 'NONE',  ( 1.000000000000000000, 0.000000000000000000, 0.000000000000000000 ) ) ;
#8803=DIRECTION ( 'NONE',  ( 0.000000000000000000, 0.000000000000000000, -1.000000000000000000 ) ) ;
#8832=CARTESIAN_POINT ( 'NONE',  ( 37.00000000000000000, 68.00000000000000000, 23.00000000000001066 ) ) ;
#8855=DIRECTION ( 'NONE',  ( 0.000000000000000000, 0.000000000000000000, -1.000000000000000000 ) ) ;
#8862=EDGE_CURVE ( 'NONE', #6976, #18143, #15528, .T. ) ;
#8877=CARTESIAN_POINT ( 'NONE',  ( -25.99999999999999645, 68.00000000000000000, -39.99999999999999289 ) ) ;
#8903=CYLINDRICAL_SURFACE ( 'NONE', #9142, 4.999999999999997335 ) ;
#8904=VECTOR ( 'NONE', #4669, 1000.000000000000000 ) ;
#8908=EDGE_LOOP ( 'NONE', ( #19080, #18947, #1693, #16671 ) ) ;
#8909=AXIS2_PLACEMENT_3D ( 'NONE', #19565, #19457, #17824 ) ;
#8923=SHAPE_REPRESENTATION ( 'Servo-Body', ( #2741 ), #6708 ) ;
#8938=DIRECTION ( 'NONE',  ( 1.000000000000000000, -0.000000000000000000, 0.000000000000000000 ) ) ;
#8961=AXIS2_PLACEMENT_3D ( 'NONE', #15487, #5803, #5583 ) ;
#8962=ORIENTED_EDGE ( 'NONE', *, *, #18444, .T. ) ;
#9020=VERTEX_POINT ( 'NONE', #1667 ) ;
#9025=DIRECTION ( 'NONE',  ( -0.000000000000000000, -1.000000000000000000, 0.000000000000000000 ) ) ;
#9041=DIRECTION ( 'NONE',  ( -0.000000000000000000, -0.000000000000000000, 1.000000000000000000 ) ) ;
#9045=VERTEX_POINT ( 'NONE', #18693 ) ;
#9055=ORIENTED_EDGE ( 'NONE', *, *, #8002, .T. ) ;
#9064=VECTOR ( 'NONE', #7905, 1000.000000000000000 ) ;
#9090=FACE_OUTER_BOUND ( 'NONE', #7357, .T. ) ;
#9105=DIRECTION ( 'NONE',  ( -1.000000000000000000, 0.000000000000000000, -0.000000000000000000 ) ) ;
#9108=LINE ( 'NONE', #20222, #15674 ) ;
#9142=AXIS2_PLACEMENT_3D ( 'NONE', #7562, #7364, #13649 ) ;
#9166=DIRECTION ( 'NONE',  ( -0.000000000000000000, -0.000000000000000000, 1.000000000000000000 ) ) ;
#9182=DIRECTION ( 'NONE',  ( -0.000000000000000000, -1.000000000000000000, 0.000000000000000000 ) ) ;
#9184=VERTEX_POINT ( 'NONE', #10516 ) ;
#9200=ORIENTED_EDGE ( 'NONE', *, *, #2109, .F. ) ;
#9262=EDGE_LOOP ( 'NONE', ( #118, #12579, #6345, #7289 ) ) ;
#9268=ORIENTED_EDGE ( 'NONE', *, *, #17446, .F. ) ;
#9347=AXIS2_PLACEMENT_3D ( 'NONE', #14448, #11464, #17843 ) ;
#9350=ORIENTED_EDGE ( 'NONE', *, *, #8426, .F. ) ;
#9380=CARTESIAN_POINT ( 'NONE',  ( -22.99999999999999645, 0.000000000000000000, -31.00000000000005684 ) ) ;
#9383=VERTEX_POINT ( 'NONE', #15584 ) ;
#9388=VECTOR ( 'NONE', #3030, 1000.000000000000000 ) ;
#9420=PRODUCT_DEFINITION_SHAPE ( 'NONE', 'NONE',  #13275 ) ;
#9429=VECTOR ( 'NONE', #2316, 1000.000000000000000 ) ;
#9451=VERTEX_POINT ( 'NONE', #8040 ) ;
#9459=CARTESIAN_POINT ( 'NONE',  ( -22.99999999999999645, 0.000000000000000000, -36.99999999999999289 ) ) ;
#9466=DIRECTION ( 'NONE',  ( 0.000000000000000000, 0.000000000000000000, -1.000000000000000000 ) ) ;
#9496=VERTEX_POINT ( 'NONE', #11222 ) ;
#9556=VECTOR ( 'NONE', #6539, 1000.000000000000000 ) ;
#9574=DIRECTION ( 'NONE',  ( -0.000000000000000000, -1.000000000000000000, 0.000000000000000000 ) ) ;
#9584=CIRCLE ( 'NONE', #3691, 5.000000000000000888 ) ;
#9610=VECTOR ( 'NONE', #12535, 1000.000000000000000 ) ;
#9636=ADVANCED_FACE ( 'NONE', ( #7814 ), #14092, .F. ) ;
#9637=CARTESIAN_POINT ( 'NONE',  ( 37.00000000000000000, 0.000000000000000000, 23.00000000000001066 ) ) ;
#9664=VECTOR ( 'NONE', #15753, 1000.000000000000000 ) ;
#9676=EDGE_LOOP ( 'NONE', ( #15033, #18476, #11282, #17689 ) ) ;
#9688=DIRECTION ( 'NONE',  ( 0.000000000000000000, 0.000000000000000000, -1.000000000000000000 ) ) ;
#9720=CARTESIAN_POINT ( 'NONE',  ( 30.99999999999999645, 68.00000000000000000, 26.00000000000001066 ) ) ;
#9726=ORIENTED_EDGE ( 'NONE', *, *, #5335, .T. ) ;
#9729=PLANE ( 'NONE',  #3435 ) ;
#9732=ORIENTED_EDGE ( 'NONE', *, *, #1513, .T. ) ;
#9733=ORIENTED_EDGE ( 'NONE', *, *, #15686, .T. ) ;
#9751=VERTEX_POINT ( 'NONE', #1904 ) ;
#9762=EDGE_CURVE ( 'NONE', #9383, #7830, #3981, .T. ) ;
#9788=EDGE_CURVE ( 'NONE', #12515, #14600, #673, .T. ) ;
#9807=EDGE_CURVE ( 'NONE', #6976, #9496, #14798, .T. ) ;
#9822=LINE ( 'NONE', #1866, #3650 ) ;
#9823=FACE_OUTER_BOUND ( 'NONE', #9676, .T. ) ;
#9834=ORIENTED_EDGE ( 'NONE', *, *, #12887, .T. ) ;
#9838=ORIENTED_EDGE ( 'NONE', *, *, #11980, .F. ) ;
#9858=ORIENTED_EDGE ( 'NONE', *, *, #62, .F. ) ;
#9900=EDGE_CURVE ( 'NONE', #19379, #19512, #14373, .T. ) ;
#9901=FACE_BOUND ( 'NONE', #2117, .T. ) ;
#9933=CARTESIAN_POINT ( 'NONE',  ( -22.99999999999999645, 68.00000000000000000, 31.00000000000003908 ) ) ;
#9960=ORIENTED_EDGE ( 'NONE', *, *, #18795, .T. ) ;
#9977=DIRECTION ( 'NONE',  ( -0.000000000000000000, -1.000000000000000000, -0.000000000000000000 ) ) ;
#9978=CARTESIAN_POINT ( 'NONE',  ( -25.99999999999999645, 68.00000000000000000, -31.00000000000003197 ) ) ;
#9997=LINE ( 'NONE', #14945, #20270 ) ;
#10013=CIRCLE ( 'NONE', #10335, 7.999999999999996447 ) ;
#10025=CARTESIAN_POINT ( 'NONE',  ( -22.99999999999999645, 0.000000000000000000, 37.00000000000002132 ) ) ;
#10039=STYLED_ITEM ( 'NONE', ( #13816 ), #1644 ) ;
#10043=EDGE_CURVE ( 'NONE', #19129, #2599, #2084, .T. ) ;
#10048=VECTOR ( 'NONE', #17457, 1000.000000000000000 ) ;
#10061=CARTESIAN_POINT ( 'NONE',  ( -40.00000000000000000, 68.00000000000000000, 26.00000000000000355 ) ) ;
#10071=CYLINDRICAL_SURFACE ( 'NONE', #4008, 8.000000000000000000 ) ;
#10075=LINE ( 'NONE', #16083, #12926 ) ;
#10167=DIRECTION ( 'NONE',  ( 1.000000000000000000, 0.000000000000000000, 0.000000000000000000 ) ) ;
#10272=CARTESIAN_POINT ( 'NONE',  ( -37.00000000000000000, 68.00000000000000000, 23.00000000000000355 ) ) ;
#10283=AXIS2_PLACEMENT_3D ( 'NONE', #12439, #17275, #6360 ) ;
#10297=CARTESIAN_POINT ( 'NONE',  ( -37.00000000000000000, 68.00000000000000000, 23.00000000000000355 ) ) ;
#10335=AXIS2_PLACEMENT_3D ( 'NONE', #19786, #9182, #4455 ) ;
#10345=UNCERTAINTY_MEASURE_WITH_UNIT (LENGTH_MEASURE( 1.000000000000000082E-05 ), #2788, 'distance_accuracy_value', 'NONE');
#10384=ADVANCED_FACE ( 'NONE', ( #5702 ), #16750, .T. ) ;
#10403=DIRECTION ( 'NONE',  ( 0.000000000000000000, 0.000000000000000000, 1.000000000000000000 ) ) ;
#10411=CARTESIAN_POINT ( 'NONE',  ( 25.99999999999999645, 68.00000000000000000, 40.00000000000002132 ) ) ;
#10422=ORIENTED_EDGE ( 'NONE', *, *, #13762, .F. ) ;
#10428=CARTESIAN_POINT ( 'NONE',  ( 26.00000000000000711, 0.000000000000000000, -31.00000000000002487 ) ) ;
#10445=DIRECTION ( 'NONE',  ( 0.000000000000000000, 0.000000000000000000, -1.000000000000000000 ) ) ;
#10456=DIRECTION ( 'NONE',  ( 0.000000000000000000, 0.000000000000000000, 1.000000000000000000 ) ) ;
#10458=ADVANCED_FACE ( 'NONE', ( #18865 ), #14135, .T. ) ;
#10462=ORIENTED_EDGE ( 'NONE', *, *, #11174, .T. ) ;
#10472=EDGE_CURVE ( 'NONE', #12727, #4894, #12811, .T. ) ;
#10487=CARTESIAN_POINT ( 'NONE',  ( -40.00000000000000000, 68.00000000000000000, 26.00000000000000355 ) ) ;
#10490=CIRCLE ( 'NONE', #1584, 4.999999999999997335 ) ;
#10493=CARTESIAN_POINT ( 'NONE',  ( -37.00000000000000000, 0.000000000000000000, -22.99999999999999645 ) ) ;
#10516=CARTESIAN_POINT ( 'NONE',  ( -22.99999999999999645, 68.00000000000000000, -36.99999999999999289 ) ) ;
#10520=CARTESIAN_POINT ( 'NONE',  ( 31.00000000000002842, 68.00000000000000000, 23.00000000000001066 ) ) ;
#10570=ORIENTED_EDGE ( 'NONE', *, *, #15686, .F. ) ;
#10585=EDGE_LOOP ( 'NONE', ( #7730, #1135, #1301, #15370 ) ) ;
#10621=SURFACE_STYLE_USAGE ( .BOTH. , #7540 ) ;
#10650=ORIENTED_EDGE ( 'NONE', *, *, #17038, .T. ) ;
#10676=DIRECTION ( 'NONE',  ( 1.000000000000000000, -0.000000000000000000, 0.000000000000000000 ) ) ;
#10715=LINE ( 'NONE', #9637, #20099 ) ;
#10718=ORIENTED_EDGE ( 'NONE', *, *, #13370, .T. ) ;
#10754=CARTESIAN_POINT ( 'NONE',  ( -25.99999999999999645, 0.000000000000000000, 40.00000000000002132 ) ) ;
#10758=EDGE_CURVE ( 'NONE', #18212, #4662, #17603, .T. ) ;
#10764=ORIENTED_EDGE ( 'NONE', *, *, #19739, .T. ) ;
#10811=DIRECTION ( 'NONE',  ( 1.000000000000000000, 0.000000000000000000, 0.000000000000000000 ) ) ;
#10839=PLANE ( 'NONE',  #16623 ) ;
#10858=CARTESIAN_POINT ( 'NONE',  ( 31.00000000000006395, 68.00000000000000000, -22.99999999999999289 ) ) ;
#10885=LINE ( 'NONE', #20141, #17059 ) ;
#10896=VECTOR ( 'NONE', #913, 1000.000000000000000 ) ;
#10912=VECTOR ( 'NONE', #13722, 1000.000000000000000 ) ;
#10980=CARTESIAN_POINT ( 'NONE',  ( -22.99999999999999645, 68.00000000000000000, -36.99999999999999289 ) ) ;
#11002=AXIS2_PLACEMENT_3D ( 'NONE', #2552, #15137, #13700 ) ;
#11010=VECTOR ( 'NONE', #16778, 1000.000000000000000 ) ;
#11037=ORIENTED_EDGE ( 'NONE', *, *, #5484, .T. ) ;
#11086=CARTESIAN_POINT ( 'NONE',  ( 23.00000000000000711, 68.00000000000000000, -31.00000000000002487 ) ) ;
#11090=EDGE_LOOP ( 'NONE', ( #12456, #1345, #12204, #3424, #4119, #6246, #1505, #16420, #11429, #13404, #6478, #7764, #9834, #18555, #10764, #16192 ) ) ;
#11135=CARTESIAN_POINT ( 'NONE',  ( -31.00000000000005684, 0.000000000000000000, 23.00000000000000355 ) ) ;
#11143=ADVANCED_FACE ( 'NONE', ( #2611 ), #8903, .F. ) ;
#11148=DIRECTION ( 'NONE',  ( -0.000000000000000000, -1.000000000000000000, -0.000000000000000000 ) ) ;
#11155=LINE ( 'NONE', #17344, #15399 ) ;
#11174=EDGE_CURVE ( 'NONE', #14748, #8326, #11155, .T. ) ;
#11202=ORIENTED_EDGE ( 'NONE', *, *, #8620, .F. ) ;
#11222=CARTESIAN_POINT ( 'NONE',  ( 23.00000000000000711, 0.000000000000000000, -31.00000000000002487 ) ) ;
#11269=EDGE_CURVE ( 'NONE', #19399, #4616, #3559, .T. ) ;
#11282=ORIENTED_EDGE ( 'NONE', *, *, #3159, .F. ) ;
#11329=ORIENTED_EDGE ( 'NONE', *, *, #13087, .F. ) ;
#11383=ORIENTED_EDGE ( 'NONE', *, *, #8862, .F. ) ;
#11420=EDGE_CURVE ( 'NONE', #4616, #2478, #5393, .T. ) ;
#11429=ORIENTED_EDGE ( 'NONE', *, *, #3838, .T. ) ;
#11446=VECTOR ( 'NONE', #8855, 1000.000000000000000 ) ;
#11448=DIRECTION ( 'NONE',  ( 0.000000000000000000, 0.000000000000000000, -1.000000000000000000 ) ) ;
#11458=LINE ( 'NONE', #13127, #10896 ) ;
#11464=DIRECTION ( 'NONE',  ( -0.000000000000000000, -1.000000000000000000, 0.000000000000000000 ) ) ;
#11508=ADVANCED_FACE ( 'NONE', ( #13729 ), #15384, .T. ) ;
#11555=VERTEX_POINT ( 'NONE', #4550 ) ;
#11558=VERTEX_POINT ( 'NONE', #11135 ) ;
#11570=DIRECTION ( 'NONE',  ( -1.156482317317875275E-15, 0.000000000000000000, -1.000000000000000000 ) ) ;
#11572=LINE ( 'NONE', #3941, #4449 ) ;
#11574=LINE ( 'NONE', #17856, #19860 ) ;
#11607=FACE_OUTER_BOUND ( 'NONE', #12717, .T. ) ;
#11621=DIRECTION ( 'NONE',  ( 0.000000000000000000, 0.000000000000000000, -1.000000000000000000 ) ) ;
#11627=VERTEX_POINT ( 'NONE', #19050 ) ;
#11681=VERTEX_POINT ( 'NONE', #6210 ) ;
#11718=LINE ( 'NONE', #16267, #6320 ) ;
#11724=DIRECTION ( 'NONE',  ( 0.000000000000000000, 0.000000000000000000, -1.000000000000000000 ) ) ;
#11727=ADVANCED_FACE ( 'NONE', ( #16412, #9901 ), #5178, .F. ) ;
#11733=LINE ( 'NONE', #15218, #11010 ) ;
#11757=PLANE ( 'NONE',  #5445 ) ;
#11775=ORIENTED_EDGE ( 'NONE', *, *, #16002, .F. ) ;
#11783=DIRECTION ( 'NONE',  ( -1.000000000000000000, -0.000000000000000000, -0.000000000000000000 ) ) ;
#11826=PLANE ( 'NONE',  #20129 ) ;
#11840=DIRECTION ( 'NONE',  ( 1.000000000000000000, -0.000000000000000000, 0.000000000000000000 ) ) ;
#11859=LINE ( 'NONE', #18116, #14161 ) ;
#11860=AXIS2_PLACEMENT_3D ( 'NONE', #2009, #5037, #12875 ) ;
#11871=VECTOR ( 'NONE', #5584, 1000.000000000000000 ) ;
#11882=LINE ( 'NONE', #12175, #11871 ) ;
#11887=DIRECTION ( 'NONE',  ( -0.000000000000000000, -1.000000000000000000, -0.000000000000000000 ) ) ;
#11893=EDGE_CURVE ( 'NONE', #7970, #7830, #12153, .T. ) ;
#11897=CARTESIAN_POINT ( 'NONE',  ( 31.00000000000002842, 0.000000000000000000, 26.00000000000001066 ) ) ;
#11914=ORIENTED_EDGE ( 'NONE', *, *, #4561, .T. ) ;
#11934=VECTOR ( 'NONE', #10167, 1000.000000000000000 ) ;
#11936=PLANE ( 'NONE',  #1939 ) ;
#11943=UNCERTAINTY_MEASURE_WITH_UNIT (LENGTH_MEASURE( 1.000000000000000082E-05 ), #6996, 'distance_accuracy_value', 'NONE');
#11949=PLANE ( 'NONE',  #653 ) ;
#11953=EDGE_CURVE ( 'NONE', #19875, #17263, #14484, .T. ) ;
#11959=DIRECTION ( 'NONE',  ( -1.000000000000000000, 0.000000000000000000, -0.000000000000000000 ) ) ;
#11980=EDGE_CURVE ( 'NONE', #7373, #20355, #10715, .T. ) ;
#11985=ORIENTED_EDGE ( 'NONE', *, *, #15665, .F. ) ;
#11998=CARTESIAN_POINT ( 'NONE',  ( -30.99999999999999645, 68.00000000000000000, -30.99999999999999289 ) ) ;
#11999=CARTESIAN_POINT ( 'NONE',  ( -37.00000000000000000, 68.00000000000000000, 23.00000000000000355 ) ) ;
#12005=VECTOR ( 'NONE', #16319, 1000.000000000000000 ) ;
#12030=DIRECTION ( 'NONE',  ( 0.000000000000000000, 0.000000000000000000, -1.000000000000000000 ) ) ;
#12031=AXIS2_PLACEMENT_3D ( 'NONE', #8203, #3465, #1885 ) ;
#12049=LINE ( 'NONE', #7404, #15466 ) ;
#12119=DIRECTION ( 'NONE',  ( 0.000000000000000000, 0.000000000000000000, -1.000000000000000000 ) ) ;
#12145=CARTESIAN_POINT ( 'NONE',  ( -30.99999999999999289, 0.000000000000000000, 31.00000000000000000 ) ) ;
#12153=LINE ( 'NONE', #18528, #6292 ) ;
#12175=CARTESIAN_POINT ( 'NONE',  ( -37.00000000000000000, 68.00000000000000000, -22.99999999999999645 ) ) ;
#12204=ORIENTED_EDGE ( 'NONE', *, *, #16568, .T. ) ;
#12218=DIRECTION ( 'NONE',  ( -0.000000000000000000, -0.000000000000000000, 1.000000000000000000 ) ) ;
#12223=DIRECTION ( 'NONE',  ( -0.000000000000000000, -1.000000000000000000, 0.000000000000000000 ) ) ;
#12236=LINE ( 'NONE', #4125, #19867 ) ;
#12238=LINE ( 'NONE', #13785, #4086 ) ;
#12260=EDGE_LOOP ( 'NONE', ( #14323, #6603, #9726, #15806 ) ) ;
#12265=DIRECTION ( 'NONE',  ( -1.000000000000000000, -0.000000000000000000, -0.000000000000000000 ) ) ;
#12299=FACE_OUTER_BOUND ( 'NONE', #3168, .T. ) ;
#12342=ORIENTED_EDGE ( 'NONE', *, *, #13087, .T. ) ;
#12348=ORIENTED_EDGE ( 'NONE', *, *, #4995, .F. ) ;
#12353=EDGE_LOOP ( 'NONE', ( #7604, #5350, #7365, #14782 ) ) ;
#12396=DIRECTION ( 'NONE',  ( 0.000000000000000000, 0.000000000000000000, 1.000000000000000000 ) ) ;
#12405=DIRECTION ( 'NONE',  ( -0.000000000000000000, -1.000000000000000000, -0.000000000000000000 ) ) ;
#12411=EDGE_CURVE ( 'NONE', #4616, #19512, #11733, .T. ) ;
#12432=CARTESIAN_POINT ( 'NONE',  ( 30.99999999999999645, 0.000000000000000000, 26.00000000000001066 ) ) ;
#12439=CARTESIAN_POINT ( 'NONE',  ( 31.00000000000004263, 68.00000000000000000, -25.99999999999999645 ) ) ;
#12447=VECTOR ( 'NONE', #12218, 1000.000000000000000 ) ;
#12456=ORIENTED_EDGE ( 'NONE', *, *, #11420, .T. ) ;
#12510=VECTOR ( 'NONE', #2469, 1000.000000000000000 ) ;
#12515=VERTEX_POINT ( 'NONE', #5939 ) ;
#12522=ORIENTED_EDGE ( 'NONE', *, *, #13349, .T. ) ;
#12535=DIRECTION ( 'NONE',  ( -0.000000000000000000, -1.000000000000000000, -0.000000000000000000 ) ) ;
#12546=PRODUCT ( 'Servo-Body', 'Servo-Body', '', ( #17440 ) ) ;
#12551=EDGE_CURVE ( 'NONE', #17102, #2599, #1990, .T. ) ;
#12555=CIRCLE ( 'NONE', #19763, 4.999999999999997335 ) ;
#12563=DIRECTION ( 'NONE',  ( 1.000000000000000000, 0.000000000000000000, -0.000000000000000000 ) ) ;
#12579=ORIENTED_EDGE ( 'NONE', *, *, #18097, .F. ) ;
#12597=DIRECTION ( 'NONE',  ( 1.000000000000000000, 0.000000000000000000, -0.000000000000000000 ) ) ;
#12618=VERTEX_POINT ( 'NONE', #14273 ) ;
#12643=CARTESIAN_POINT ( 'NONE',  ( 23.00000000000001066, 68.00000000000000000, -36.99999999999999289 ) ) ;
#12693=CIRCLE ( 'NONE', #13669, 4.999999999999997335 ) ;
#12717=EDGE_LOOP ( 'NONE', ( #7004, #6335, #15367, #2255 ) ) ;
#12725=CARTESIAN_POINT ( 'NONE',  ( -22.99999999999999645, 68.00000000000000000, 37.00000000000002132 ) ) ;
#12727=VERTEX_POINT ( 'NONE', #943 ) ;
#12737=ORIENTED_EDGE ( 'NONE', *, *, #5893, .F. ) ;
#12754=FACE_OUTER_BOUND ( 'NONE', #1054, .T. ) ;
#12760=LINE ( 'NONE', #4917, #9064 ) ;
#12766=EDGE_LOOP ( 'NONE', ( #16079, #6973, #8127, #4850 ) ) ;
#12778=PLANE ( 'NONE',  #19161 ) ;
#12806=ORIENTED_EDGE ( 'NONE', *, *, #16098, .T. ) ;
#12811=LINE ( 'NONE', #19069, #2120 ) ;
#12875=DIRECTION ( 'NONE',  ( -1.000000000000000000, 0.000000000000000000, -0.000000000000000000 ) ) ;
#12882=DIRECTION ( 'NONE',  ( -0.000000000000000000, -1.000000000000000000, -0.000000000000000000 ) ) ;
#12887=EDGE_CURVE ( 'NONE', #14748, #11627, #15403, .T. ) ;
#12926=VECTOR ( 'NONE', #12978, 1000.000000000000000 ) ;
#12978=DIRECTION ( 'NONE',  ( -0.000000000000000000, -1.000000000000000000, -0.000000000000000000 ) ) ;
#12999=AXIS2_PLACEMENT_3D ( 'NONE', #18296, #15110, #19824 ) ;
#13009=CARTESIAN_POINT ( 'NONE',  ( -31.00000000000003197, 0.000000000000000000, -22.99999999999999645 ) ) ;
#13014=AXIS2_PLACEMENT_3D ( 'NONE', #17125, #20314, #12597 ) ;
#13022=ORIENTED_EDGE ( 'NONE', *, *, #8620, .T. ) ;
#13026=DIRECTION ( 'NONE',  ( 0.000000000000000000, 0.000000000000000000, -1.000000000000000000 ) ) ;
#13040=CARTESIAN_POINT ( 'NONE',  ( 37.00000000000000000, 68.00000000000000000, 23.00000000000001066 ) ) ;
#13071=DIRECTION ( 'NONE',  ( -0.000000000000000000, -1.000000000000000000, -0.000000000000000000 ) ) ;
#13083=LINE ( 'NONE', #10411, #12510 ) ;
#13087=EDGE_CURVE ( 'NONE', #2627, #19923, #11572, .T. ) ;
#13096=DIRECTION ( 'NONE',  ( -1.000000000000000000, 0.000000000000000000, -0.000000000000000000 ) ) ;
#13102=DIRECTION ( 'NONE',  ( 0.000000000000000000, 0.000000000000000000, -1.000000000000000000 ) ) ;
#13112=CARTESIAN_POINT ( 'NONE',  ( -22.99999999999999645, 0.000000000000000000, 31.00000000000003908 ) ) ;
#13121=DIRECTION ( 'NONE',  ( -0.000000000000000000, -1.000000000000000000, -0.000000000000000000 ) ) ;
#13127=CARTESIAN_POINT ( 'NONE',  ( 31.00000000000006395, 0.000000000000000000, -22.99999999999999289 ) ) ;
#13134=DIRECTION ( 'NONE',  ( 0.000000000000000000, 0.000000000000000000, 1.000000000000000000 ) ) ;
#13175=DIRECTION ( 'NONE',  ( 0.000000000000000000, 0.000000000000000000, -1.000000000000000000 ) ) ;
#13183=LINE ( 'NONE', #16284, #11934 ) ;
#13205=DIRECTION ( 'NONE',  ( 0.000000000000000000, 0.000000000000000000, -1.000000000000000000 ) ) ;
#13257=EDGE_CURVE ( 'NONE', #12618, #1696, #14312, .T. ) ;
#13264=ADVANCED_FACE ( 'NONE', ( #18827 ), #12778, .F. ) ;
#13275=PRODUCT_DEFINITION ( 'UNKNOWN', '', #16561, #3702 ) ;
#13312=CARTESIAN_POINT ( 'NONE',  ( -25.99999999999999645, 68.00000000000000000, 40.00000000000002132 ) ) ;
#13314=ADVANCED_FACE ( 'NONE', ( #685 ), #3600, .F. ) ;
#13339=VECTOR ( 'NONE', #7563, 1000.000000000000000 ) ;
#13349=EDGE_CURVE ( 'NONE', #7572, #7705, #14411, .T. ) ;
#13356=VERTEX_POINT ( 'NONE', #14616 ) ;
#13370=EDGE_CURVE ( 'NONE', #9751, #17102, #5678, .T. ) ;
#13404=ORIENTED_EDGE ( 'NONE', *, *, #3159, .T. ) ;
#13411=CARTESIAN_POINT ( 'NONE',  ( 40.00000000000000000, 0.000000000000000000, -25.99999999999999645 ) ) ;
#13489=DIRECTION ( 'NONE',  ( 0.000000000000000000, 0.000000000000000000, -1.000000000000000000 ) ) ;
#13649=DIRECTION ( 'NONE',  ( 0.000000000000000000, 0.000000000000000000, -1.000000000000000000 ) ) ;
#13650=MECHANICAL_DESIGN_GEOMETRIC_PRESENTATION_REPRESENTATION('',(#10039),#14637);
#13663=ORIENTED_EDGE ( 'NONE', *, *, #3429, .T. ) ;
#13669=AXIS2_PLACEMENT_3D ( 'NONE', #5184, #6736, #13026 ) ;
#13700=DIRECTION ( 'NONE',  ( 0.000000000000000000, 0.000000000000000000, -1.000000000000000000 ) ) ;
#13721=LINE ( 'NONE', #1207, #2080 ) ;
#13722=DIRECTION ( 'NONE',  ( -1.156482317317875275E-15, 0.000000000000000000, -1.000000000000000000 ) ) ;
#13729=FACE_OUTER_BOUND ( 'NONE', #14111, .T. ) ;
#13736=EDGE_CURVE ( 'NONE', #14418, #11558, #16129, .T. ) ;
#13762=EDGE_CURVE ( 'NONE', #503, #17973, #8280, .T. ) ;
#13769=LINE ( 'NONE', #2538, #12447 ) ;
#13774=ORIENTED_EDGE ( 'NONE', *, *, #10472, .T. ) ;
#13785=CARTESIAN_POINT ( 'NONE',  ( -25.99999999999999645, 68.00000000000000000, 31.00000000000003908 ) ) ;
#13794=ADVANCED_FACE ( 'NONE', ( #17844 ), #16426, .T. ) ;
#13806=ORIENTED_EDGE ( 'NONE', *, *, #16568, .F. ) ;
#13816=PRESENTATION_STYLE_ASSIGNMENT (( #10621 ) ) ;
#13882=VERTEX_POINT ( 'NONE', #6636 ) ;
#13921=CARTESIAN_POINT ( 'NONE',  ( -37.00000000000000000, 0.000000000000000000, 23.00000000000000355 ) ) ;
#13945=ADVANCED_FACE ( 'NONE', ( #9090 ), #1212, .F. ) ;
#14013=LINE ( 'NONE', #17304, #15856 ) ;
#14048=ORIENTED_EDGE ( 'NONE', *, *, #17690, .F. ) ;
#14072=CARTESIAN_POINT ( 'NONE',  ( -25.99999999999999645, 0.000000000000000000, -31.00000000000003197 ) ) ;
#14080=PLANE ( 'NONE',  #5370 ) ;
#14092=PLANE ( 'NONE',  #6150 ) ;
#14107=ORIENTED_EDGE ( 'NONE', *, *, #14596, .T. ) ;
#14111=EDGE_LOOP ( 'NONE', ( #3570, #14761, #5258, #12522 ) ) ;
#14112=ORIENTED_EDGE ( 'NONE', *, *, #16621, .T. ) ;
#14135=PLANE ( 'NONE',  #13014 ) ;
#14161=VECTOR ( 'NONE', #16614, 1000.000000000000000 ) ;
#14220=EDGE_CURVE ( 'NONE', #17973, #16787, #7020, .T. ) ;
#14223=AXIS2_PLACEMENT_3D ( 'NONE', #9978, #380, #11621 ) ;
#14273=CARTESIAN_POINT ( 'NONE',  ( -22.99999999999999645, 68.00000000000000000, 37.00000000000002132 ) ) ;
#14292=ADVANCED_FACE ( 'NONE', ( #6159 ), #11757, .T. ) ;
#14312=LINE ( 'NONE', #17303, #18492 ) ;
#14316=DIRECTION ( 'NONE',  ( 0.000000000000000000, 0.000000000000000000, -1.000000000000000000 ) ) ;
#14323=ORIENTED_EDGE ( 'NONE', *, *, #6448, .F. ) ;
#14362=LINE ( 'NONE', #18683, #6548 ) ;
#14363=CARTESIAN_POINT ( 'NONE',  ( 22.99999999999999289, 0.000000000000000000, 37.00000000000002132 ) ) ;
#14373=CIRCLE ( 'NONE', #17669, 4.999999999999997335 ) ;
#14411=LINE ( 'NONE', #14508, #19808 ) ;
#14416=EDGE_CURVE ( 'NONE', #3148, #20355, #17566, .T. ) ;
#14418=VERTEX_POINT ( 'NONE', #16060 ) ;
#14426=DIRECTION ( 'NONE',  ( -0.000000000000000000, -1.000000000000000000, -0.000000000000000000 ) ) ;
#14444=CARTESIAN_POINT ( 'NONE',  ( 22.99999999999999645, 68.00000000000000000, 31.00000000000006750 ) ) ;
#14445=VERTEX_POINT ( 'NONE', #1795 ) ;
#14448=CARTESIAN_POINT ( 'NONE',  ( 30.99999999999999645, 0.000000000000000000, 31.00000000000001066 ) ) ;
#14459=CARTESIAN_POINT ( 'NONE',  ( -23.00000000000000000, 0.000000000000000000, -31.00000000000005684 ) ) ;
#14481=VECTOR ( 'NONE', #3955, 1000.000000000000000 ) ;
#14484=LINE ( 'NONE', #7997, #19118 ) ;
#14508=CARTESIAN_POINT ( 'NONE',  ( 31.00000000000002842, 68.00000000000000000, 23.00000000000001066 ) ) ;
#14541=ORIENTED_EDGE ( 'NONE', *, *, #10043, .T. ) ;
#14549=LINE ( 'NONE', #17647, #3149 ) ;
#14550=CARTESIAN_POINT ( 'NONE',  ( -31.00000000000005684, 68.00000000000000000, 23.00000000000000355 ) ) ;
#14577=AXIS2_PLACEMENT_3D ( 'NONE', #13040, #19295, #13134 ) ;
#14596=EDGE_CURVE ( 'NONE', #19875, #3145, #19910, .T. ) ;
#14600=VERTEX_POINT ( 'NONE', #7473 ) ;
#14606=PLANE ( 'NONE',  #11860 ) ;
#14616=CARTESIAN_POINT ( 'NONE',  ( 25.99999999999999645, 68.00000000000000000, 31.00000000000004619 ) ) ;
#14637=( GEOMETRIC_REPRESENTATION_CONTEXT ( 3 ) GLOBAL_UNCERTAINTY_ASSIGNED_CONTEXT ( ( #10345 ) ) GLOBAL_UNIT_ASSIGNED_CONTEXT ( ( #2788, #20087, #1201 ) ) REPRESENTATION_CONTEXT ( 'NONE', 'WORKASPACE' ) );
#14652=ORIENTED_EDGE ( 'NONE', *, *, #13257, .F. ) ;
#14655=PLANE ( 'NONE',  #19436 ) ;
#14664=VECTOR ( 'NONE', #6019, 1000.000000000000000 ) ;
#14692=LINE ( 'NONE', #8877, #19492 ) ;
#14716=CARTESIAN_POINT ( 'NONE',  ( 25.99999999999999645, 68.00000000000000000, 40.00000000000002132 ) ) ;
#14748=VERTEX_POINT ( 'NONE', #9720 ) ;
#14753=ORIENTED_EDGE ( 'NONE', *, *, #17356, .T. ) ;
#14761=ORIENTED_EDGE ( 'NONE', *, *, #7789, .F. ) ;
#14782=ORIENTED_EDGE ( 'NONE', *, *, #62, .T. ) ;
#14787=CIRCLE ( 'NONE', #5906, 7.999999999999996447 ) ;
#14797=DIRECTION ( 'NONE',  ( -0.000000000000000000, -1.000000000000000000, -0.000000000000000000 ) ) ;
#14798=LINE ( 'NONE', #871, #3847 ) ;
#14828=LINE ( 'NONE', #10493, #17760 ) ;
#14852=ORIENTED_EDGE ( 'NONE', *, *, #3429, .F. ) ;
#14870=ORIENTED_EDGE ( 'NONE', *, *, #2630, .F. ) ;
#14915=CARTESIAN_POINT ( 'NONE',  ( -31.00000000000002842, 0.000000000000000000, -25.99999999999999645 ) ) ;
#14938=FACE_OUTER_BOUND ( 'NONE', #18384, .T. ) ;
#14943=VECTOR ( 'NONE', #7803, 1000.000000000000000 ) ;
#14945=CARTESIAN_POINT ( 'NONE',  ( 31.00000000000006395, 68.00000000000000000, -22.99999999999999289 ) ) ;
#14991=CIRCLE ( 'NONE', #6108, 8.000000000000000000 ) ;
#15033=ORIENTED_EDGE ( 'NONE', *, *, #19685, .T. ) ;
#15042=FACE_OUTER_BOUND ( 'NONE', #10585, .T. ) ;
#15049=CARTESIAN_POINT ( 'NONE',  ( -25.99999999999999645, 68.00000000000000000, 40.00000000000002132 ) ) ;
#15067=LINE ( 'NONE', #8561, #3817 ) ;
#15070=ADVANCED_FACE ( 'NONE', ( #404 ), #2037, .T. ) ;
#15087=ORIENTED_EDGE ( 'NONE', *, *, #2342, .T. ) ;
#15110=DIRECTION ( 'NONE',  ( -0.000000000000000000, -1.000000000000000000, 0.000000000000000000 ) ) ;
#15123=FACE_OUTER_BOUND ( 'NONE', #19621, .T. ) ;
#15137=DIRECTION ( 'NONE',  ( -0.000000000000000000, -1.000000000000000000, -0.000000000000000000 ) ) ;
#15218=CARTESIAN_POINT ( 'NONE',  ( 26.00000000000001066, 68.00000000000000000, -31.00000000000002487 ) ) ;
#15229=DIRECTION ( 'NONE',  ( -0.000000000000000000, -0.000000000000000000, 1.000000000000000000 ) ) ;
#15239=DIRECTION ( 'NONE',  ( 0.000000000000000000, 0.000000000000000000, -1.000000000000000000 ) ) ;
#15256=AXIS2_PLACEMENT_3D ( 'NONE', #15049, #1867, #11959 ) ;
#15326=EDGE_CURVE ( 'NONE', #1696, #16787, #2224, .T. ) ;
#15344=ORIENTED_EDGE ( 'NONE', *, *, #1817, .F. ) ;
#15364=LINE ( 'NONE', #4529, #3742 ) ;
#15367=ORIENTED_EDGE ( 'NONE', *, *, #8426, .T. ) ;
#15370=ORIENTED_EDGE ( 'NONE', *, *, #18695, .T. ) ;
#15378=SURFACE_STYLE_FILL_AREA ( #7239 ) ;
#15384=CYLINDRICAL_SURFACE ( 'NONE', #8961, 8.000000000000000000 ) ;
#15394=FACE_OUTER_BOUND ( 'NONE', #9262, .T. ) ;
#15399=VECTOR ( 'NONE', #3227, 1000.000000000000000 ) ;
#15403=LINE ( 'NONE', #1232, #13339 ) ;
#15417=EDGE_CURVE ( 'NONE', #6058, #7572, #14991, .T. ) ;
#15466=VECTOR ( 'NONE', #9041, 1000.000000000000000 ) ;
#15487=CARTESIAN_POINT ( 'NONE',  ( 30.99999999999999645, 68.00000000000000000, 31.00000000000001066 ) ) ;
#15516=DIRECTION ( 'NONE',  ( 1.000000000000000000, 0.000000000000000000, -1.156482317317883755E-15 ) ) ;
#15522=ORIENTED_EDGE ( 'NONE', *, *, #561, .F. ) ;
#15528=LINE ( 'NONE', #18604, #1474 ) ;
#15584=CARTESIAN_POINT ( 'NONE',  ( 40.00000000000000000, 0.000000000000000000, 26.00000000000000355 ) ) ;
#15587=VECTOR ( 'NONE', #3741, 1000.000000000000000 ) ;
#15623=DIRECTION ( 'NONE',  ( 1.156482317317883755E-15, -0.000000000000000000, 1.000000000000000000 ) ) ;
#15665=EDGE_CURVE ( 'NONE', #7572, #3235, #2271, .T. ) ;
#15667=ORIENTED_EDGE ( 'NONE', *, *, #12411, .T. ) ;
#15674=VECTOR ( 'NONE', #20002, 1000.000000000000000 ) ;
#15684=CARTESIAN_POINT ( 'NONE',  ( -30.99999999999999289, 0.000000000000000000, 31.00000000000000000 ) ) ;
#15686=EDGE_CURVE ( 'NONE', #9496, #18212, #11574, .T. ) ;
#15710=EDGE_CURVE ( 'NONE', #14418, #18003, #10013, .T. ) ;
#15733=ORIENTED_EDGE ( 'NONE', *, *, #20174, .F. ) ;
#15752=PLANE ( 'NONE',  #10283 ) ;
#15753=DIRECTION ( 'NONE',  ( 1.000000000000000000, 0.000000000000000000, 0.000000000000000000 ) ) ;
#15790=VECTOR ( 'NONE', #9466, 1000.000000000000000 ) ;
#15793=AXIS2_PLACEMENT_3D ( 'NONE', #3502, #6697, #6813 ) ;
#15806=ORIENTED_EDGE ( 'NONE', *, *, #19952, .T. ) ;
#15856=VECTOR ( 'NONE', #3503, 1000.000000000000000 ) ;
#15916=VECTOR ( 'NONE', #8462, 1000.000000000000000 ) ;
#15923=CARTESIAN_POINT ( 'NONE',  ( -40.00000000000000000, 0.000000000000000000, 26.00000000000000355 ) ) ;
#15958=DIRECTION ( 'NONE',  ( 1.000000000000000000, 0.000000000000000000, 0.000000000000000000 ) ) ;
#16002=EDGE_CURVE ( 'NONE', #18143, #18212, #4018, .T. ) ;
#16005=ORIENTED_EDGE ( 'NONE', *, *, #11269, .F. ) ;
#16032=CIRCLE ( 'NONE', #1166, 4.999999999999997335 ) ;
#16046=CARTESIAN_POINT ( 'NONE',  ( 31.00000000000004263, 0.000000000000000000, -25.99999999999999645 ) ) ;
#16060=CARTESIAN_POINT ( 'NONE',  ( -31.00000000000005684, 68.00000000000000000, 23.00000000000000355 ) ) ;
#16065=LINE ( 'NONE', #10061, #3033 ) ;
#16066=CARTESIAN_POINT ( 'NONE',  ( 25.99999999999999645, 68.00000000000000000, 40.00000000000002132 ) ) ;
#16079=ORIENTED_EDGE ( 'NONE', *, *, #14220, .F. ) ;
#16083=CARTESIAN_POINT ( 'NONE',  ( -23.00000000000000000, 68.00000000000000000, -31.00000000000005684 ) ) ;
#16098=EDGE_CURVE ( 'NONE', #3235, #3148, #3393, .T. ) ;
#16124=ORIENTED_EDGE ( 'NONE', *, *, #11980, .T. ) ;
#16129=LINE ( 'NONE', #14550, #15587 ) ;
#16132=CARTESIAN_POINT ( 'NONE',  ( 26.00000000000000711, 68.00000000000000000, -31.00000000000002487 ) ) ;
#16136=DIRECTION ( 'NONE',  ( 0.000000000000000000, 0.000000000000000000, -1.000000000000000000 ) ) ;
#16192=ORIENTED_EDGE ( 'NONE', *, *, #11269, .T. ) ;
#16200=VECTOR ( 'NONE', #5454, 1000.000000000000000 ) ;
#16267=CARTESIAN_POINT ( 'NONE',  ( -40.00000000000000000, 0.000000000000000000, 26.00000000000000355 ) ) ;
#16279=ADVANCED_FACE ( 'NONE', ( #20042 ), #11936, .T. ) ;
#16284=CARTESIAN_POINT ( 'NONE',  ( -25.99999999999999645, 68.00000000000000000, 40.00000000000002132 ) ) ;
#16319=DIRECTION ( 'NONE',  ( -0.000000000000000000, -1.000000000000000000, -0.000000000000000000 ) ) ;
#16332=CARTESIAN_POINT ( 'NONE',  ( 37.00000000000000000, 0.000000000000000000, 23.00000000000001066 ) ) ;
#16412=FACE_OUTER_BOUND ( 'NONE', #11090, .T. ) ;
#16420=ORIENTED_EDGE ( 'NONE', *, *, #5067, .T. ) ;
#16426=PLANE ( 'NONE',  #14577 ) ;
#16517=EDGE_LOOP ( 'NONE', ( #4257, #17147, #17831, #8962 ) ) ;
#16518=DIRECTION ( 'NONE',  ( 0.000000000000000000, -0.000000000000000000, -1.000000000000000000 ) ) ;
#16523=EDGE_CURVE ( 'NONE', #3146, #13356, #13083, .T. ) ;
#16561=PRODUCT_DEFINITION_FORMATION_WITH_SPECIFIED_SOURCE ( 'ANY', '', #12546, .NOT_KNOWN. ) ;
#16568=EDGE_CURVE ( 'NONE', #8069, #13882, #11859, .T. ) ;
#16590=CARTESIAN_POINT ( 'NONE',  ( -22.99999999999999645, 68.00000000000000000, 37.00000000000002132 ) ) ;
#16614=DIRECTION ( 'NONE',  ( -0.000000000000000000, -0.000000000000000000, 1.000000000000000000 ) ) ;
#16621=EDGE_CURVE ( 'NONE', #3581, #11558, #19023, .T. ) ;
#16623=AXIS2_PLACEMENT_3D ( 'NONE', #18759, #12396, #2995 ) ;
#16656=LINE ( 'NONE', #11897, #14481 ) ;
#16671=ORIENTED_EDGE ( 'NONE', *, *, #7789, .T. ) ;
#16707=CARTESIAN_POINT ( 'NONE',  ( -30.99999999999999289, 68.00000000000000000, 31.00000000000000000 ) ) ;
#16750=CYLINDRICAL_SURFACE ( 'NONE', #137, 8.000000000000000000 ) ;
#16778=DIRECTION ( 'NONE',  ( -0.000000000000000000, -1.000000000000000000, -0.000000000000000000 ) ) ;
#16780=DIRECTION ( 'NONE',  ( -7.709882115452498874E-16, 0.000000000000000000, -1.000000000000000000 ) ) ;
#16787=VERTEX_POINT ( 'NONE', #7478 ) ;
#16836=ADVANCED_FACE ( 'NONE', ( #12299 ), #4574, .T. ) ;
#16850=APPLICATION_CONTEXT ( 'automotive_design' ) ;
#16860=ORIENTED_EDGE ( 'NONE', *, *, #17192, .F. ) ;
#16890=ORIENTED_EDGE ( 'NONE', *, *, #4561, .F. ) ;
#16898=DIRECTION ( 'NONE',  ( -0.000000000000000000, -1.000000000000000000, -0.000000000000000000 ) ) ;
#16904=DIRECTION ( 'NONE',  ( -1.000000000000000000, -0.000000000000000000, -0.000000000000000000 ) ) ;
#16914=ORIENTED_EDGE ( 'NONE', *, *, #7451, .F. ) ;
#17014=VECTOR ( 'NONE', #11724, 1000.000000000000000 ) ;
#17015=ORIENTED_EDGE ( 'NONE', *, *, #20174, .T. ) ;
#17038=EDGE_CURVE ( 'NONE', #16787, #11555, #8189, .T. ) ;
#17059=VECTOR ( 'NONE', #18615, 1000.000000000000000 ) ;
#17102=VERTEX_POINT ( 'NONE', #7223 ) ;
#17125=CARTESIAN_POINT ( 'NONE',  ( -37.00000000000000000, 68.00000000000000000, -22.99999999999999645 ) ) ;
#17134=DIRECTION ( 'NONE',  ( 0.000000000000000000, 0.000000000000000000, -1.000000000000000000 ) ) ;
#17135=LINE ( 'NONE', #10754, #18440 ) ;
#17147=ORIENTED_EDGE ( 'NONE', *, *, #13349, .F. ) ;
#17154=LINE ( 'NONE', #14072, #9388 ) ;
#17171=VERTEX_POINT ( 'NONE', #2770 ) ;
#17192=EDGE_CURVE ( 'NONE', #4894, #2001, #14013, .T. ) ;
#17210=CARTESIAN_POINT ( 'NONE',  ( 22.99999999999999645, 68.00000000000000000, 31.00000000000006750 ) ) ;
#17243=DIRECTION ( 'NONE',  ( 1.000000000000000000, 0.000000000000000000, 0.000000000000000000 ) ) ;
#17263=VERTEX_POINT ( 'NONE', #4632 ) ;
#17275=DIRECTION ( 'NONE',  ( 0.000000000000000000, 0.000000000000000000, 1.000000000000000000 ) ) ;
#17302=CARTESIAN_POINT ( 'NONE',  ( -37.00000000000000000, 0.000000000000000000, 23.00000000000000355 ) ) ;
#17303=CARTESIAN_POINT ( 'NONE',  ( -22.99999999999999645, 68.00000000000000000, 37.00000000000002132 ) ) ;
#17304=CARTESIAN_POINT ( 'NONE',  ( -40.00000000000000000, 0.000000000000000000, 26.00000000000000355 ) ) ;
#17306=EDGE_CURVE ( 'NONE', #2001, #7513, #12555, .T. ) ;
#17339=ORIENTED_EDGE ( 'NONE', *, *, #18314, .F. ) ;
#17344=CARTESIAN_POINT ( 'NONE',  ( 30.99999999999999645, 68.00000000000000000, 26.00000000000001066 ) ) ;
#17351=ORIENTED_EDGE ( 'NONE', *, *, #2342, .F. ) ;
#17356=EDGE_CURVE ( 'NONE', #11627, #9383, #6814, .T. ) ;
#17429=ORIENTED_EDGE ( 'NONE', *, *, #13736, .F. ) ;
#17438=DIRECTION ( 'NONE',  ( -1.000000000000000000, 0.000000000000000000, -5.782411586589400040E-16 ) ) ;
#17440=PRODUCT_CONTEXT ( 'NONE', #16850, 'mechanical' ) ;
#17446=EDGE_CURVE ( 'NONE', #17263, #12727, #18403, .T. ) ;
#17447=ORIENTED_EDGE ( 'NONE', *, *, #17690, .T. ) ;
#17457=DIRECTION ( 'NONE',  ( -0.000000000000000000, -1.000000000000000000, -0.000000000000000000 ) ) ;
#17474=ORIENTED_EDGE ( 'NONE', *, *, #18170, .F. ) ;
#17566=LINE ( 'NONE', #354, #10048 ) ;
#17603=LINE ( 'NONE', #9459, #5439 ) ;
#17638=CIRCLE ( 'NONE', #6467, 5.000000000000000888 ) ;
#17647=CARTESIAN_POINT ( 'NONE',  ( -25.99999999999999645, 0.000000000000000000, 40.00000000000002132 ) ) ;
#17669=AXIS2_PLACEMENT_3D ( 'NONE', #2119, #8435, #13175 ) ;
#17689=ORIENTED_EDGE ( 'NONE', *, *, #2109, .T. ) ;
#17690=EDGE_CURVE ( 'NONE', #19061, #4894, #11718, .T. ) ;
#17695=ORIENTED_EDGE ( 'NONE', *, *, #9900, .T. ) ;
#17710=ORIENTED_EDGE ( 'NONE', *, *, #5973, .T. ) ;
#17738=CARTESIAN_POINT ( 'NONE',  ( -30.99999999999999645, 0.000000000000000000, -30.99999999999999289 ) ) ;
#17757=LINE ( 'NONE', #16046, #1344 ) ;
#17760=VECTOR ( 'NONE', #8763, 1000.000000000000000 ) ;
#17788=DIRECTION ( 'NONE',  ( 0.000000000000000000, 0.000000000000000000, -1.000000000000000000 ) ) ;
#17822=DIRECTION ( 'NONE',  ( 1.000000000000000000, -0.000000000000000000, 0.000000000000000000 ) ) ;
#17824=DIRECTION ( 'NONE',  ( 0.000000000000000000, -0.000000000000000000, -1.000000000000000000 ) ) ;
#17831=ORIENTED_EDGE ( 'NONE', *, *, #15665, .T. ) ;
#17843=DIRECTION ( 'NONE',  ( 0.000000000000000000, 0.000000000000000000, -1.000000000000000000 ) ) ;
#17844=FACE_OUTER_BOUND ( 'NONE', #18778, .T. ) ;
#17856=CARTESIAN_POINT ( 'NONE',  ( 23.00000000000000711, 0.000000000000000000, -31.00000000000002487 ) ) ;
#17859=VECTOR ( 'NONE', #430, 1000.000000000000000 ) ;
#17860=AXIS2_PLACEMENT_3D ( 'NONE', #17870, #19220, #8497 ) ;
#17870=CARTESIAN_POINT ( 'NONE',  ( 31.00000000000000711, 68.00000000000000000, -30.99999999999999289 ) ) ;
#17890=ORIENTED_EDGE ( 'NONE', *, *, #3948, .F. ) ;
#17907=ORIENTED_EDGE ( 'NONE', *, *, #8862, .T. ) ;
#17914=ORIENTED_EDGE ( 'NONE', *, *, #1664, .F. ) ;
#17920=DIRECTION ( 'NONE',  ( -0.000000000000000000, -1.000000000000000000, -0.000000000000000000 ) ) ;
#17957=EDGE_CURVE ( 'NONE', #7830, #19379, #17757, .T. ) ;
#17966=EDGE_LOOP ( 'NONE', ( #12342, #1841, #7576, #240 ) ) ;
#17973=VERTEX_POINT ( 'NONE', #242 ) ;
#17992=DIRECTION ( 'NONE',  ( 0.000000000000000000, 0.000000000000000000, -1.000000000000000000 ) ) ;
#18003=VERTEX_POINT ( 'NONE', #9933 ) ;
#18046=CARTESIAN_POINT ( 'NONE',  ( -30.99999999999999289, 68.00000000000000000, 31.00000000000000000 ) ) ;
#18097=EDGE_CURVE ( 'NONE', #9020, #3581, #4393, .T. ) ;
#18107=FACE_OUTER_BOUND ( 'NONE', #3635, .T. ) ;
#18115=PLANE ( 'NONE',  #15256 ) ;
#18116=CARTESIAN_POINT ( 'NONE',  ( -25.99999999999999645, 68.00000000000000000, -31.00000000000003197 ) ) ;
#18135=CARTESIAN_POINT ( 'NONE',  ( 30.99999999999999645, 68.00000000000000000, 31.00000000000001066 ) ) ;
#18143=VERTEX_POINT ( 'NONE', #12643 ) ;
#18153=CARTESIAN_POINT ( 'NONE',  ( -30.99999999999999289, 68.00000000000000000, 31.00000000000000000 ) ) ;
#18160=ADVANCED_FACE ( 'NONE', ( #12754 ), #15752, .F. ) ;
#18170=EDGE_CURVE ( 'NONE', #14445, #2001, #4815, .T. ) ;
#18190=ADVANCED_FACE ( 'NONE', ( #1484 ), #14080, .F. ) ;
#18212=VERTEX_POINT ( 'NONE', #20142 ) ;
#18217=PLANE ( 'NONE',  #7267 ) ;
#18221=CARTESIAN_POINT ( 'NONE',  ( -30.99999999999999645, 68.00000000000000000, -30.99999999999999289 ) ) ;
#18226=DIRECTION ( 'NONE',  ( -0.000000000000000000, -1.000000000000000000, -0.000000000000000000 ) ) ;
#18227=CIRCLE ( 'NONE', #9347, 8.000000000000000000 ) ;
#18269=DIRECTION ( 'NONE',  ( -0.000000000000000000, -1.000000000000000000, -0.000000000000000000 ) ) ;
#18295=ORIENTED_EDGE ( 'NONE', *, *, #5067, .F. ) ;
#18296=CARTESIAN_POINT ( 'NONE',  ( -30.99999999999999645, 0.000000000000000000, -30.99999999999999289 ) ) ;
#18314=EDGE_CURVE ( 'NONE', #12727, #14445, #16065, .T. ) ;
#18384=EDGE_LOOP ( 'NONE', ( #17695, #8319, #16005, #2070 ) ) ;
#18403=LINE ( 'NONE', #19841, #1011 ) ;
#18405=ORIENTED_EDGE ( 'NONE', *, *, #2391, .F. ) ;
#18435=EDGE_LOOP ( 'NONE', ( #3578, #8242, #17890, #14753 ) ) ;
#18440=VECTOR ( 'NONE', #17243, 1000.000000000000000 ) ;
#18444=EDGE_CURVE ( 'NONE', #3235, #7373, #6832, .T. ) ;
#18474=CARTESIAN_POINT ( 'NONE',  ( 40.00000000000000000, 68.00000000000000000, 26.00000000000000355 ) ) ;
#18476=ORIENTED_EDGE ( 'NONE', *, *, #18695, .F. ) ;
#18485=ORIENTED_EDGE ( 'NONE', *, *, #6871, .T. ) ;
#18489=ADVANCED_FACE ( 'NONE', ( #15123 ), #1170, .F. ) ;
#18492=VECTOR ( 'NONE', #18940, 1000.000000000000000 ) ;
#18528=CARTESIAN_POINT ( 'NONE',  ( 40.00000000000000000, 68.00000000000000000, -25.99999999999999645 ) ) ;
#18555=ORIENTED_EDGE ( 'NONE', *, *, #3948, .T. ) ;
#18583=LINE ( 'NONE', #18977, #2966 ) ;
#18604=CARTESIAN_POINT ( 'NONE',  ( 23.00000000000000711, 68.00000000000000000, -31.00000000000002487 ) ) ;
#18615=DIRECTION ( 'NONE',  ( -0.000000000000000000, -0.000000000000000000, 1.000000000000000000 ) ) ;
#18628=ORIENTED_EDGE ( 'NONE', *, *, #9762, .F. ) ;
#18683=CARTESIAN_POINT ( 'NONE',  ( -37.00000000000000000, 68.00000000000000000, 23.00000000000000355 ) ) ;
#18693=CARTESIAN_POINT ( 'NONE',  ( -25.99999999999999645, 0.000000000000000000, 40.00000000000002132 ) ) ;
#18695=EDGE_CURVE ( 'NONE', #3146, #12515, #8114, .T. ) ;
#18706=ORIENTED_EDGE ( 'NONE', *, *, #18170, .T. ) ;
#18739=ORIENTED_EDGE ( 'NONE', *, *, #19260, .T. ) ;
#18751=VERTEX_POINT ( 'NONE', #7896 ) ;
#18759=CARTESIAN_POINT ( 'NONE',  ( -40.00000000000000000, 68.00000000000000000, -25.99999999999999645 ) ) ;
#18778=EDGE_LOOP ( 'NONE', ( #9838, #3953, #12806, #2389 ) ) ;
#18795=EDGE_CURVE ( 'NONE', #7705, #7373, #6261, .T. ) ;
#18809=ORIENTED_EDGE ( 'NONE', *, *, #7600, .T. ) ;
#18827=FACE_OUTER_BOUND ( 'NONE', #17966, .T. ) ;
#18865=FACE_OUTER_BOUND ( 'NONE', #12260, .T. ) ;
#18902=FACE_OUTER_BOUND ( 'NONE', #6195, .T. ) ;
#18910=ORIENTED_EDGE ( 'NONE', *, *, #10472, .F. ) ;
#18940=DIRECTION ( 'NONE',  ( 1.000000000000000000, 0.000000000000000000, 0.000000000000000000 ) ) ;
#18947=ORIENTED_EDGE ( 'NONE', *, *, #15326, .F. ) ;
#18974=ADVANCED_FACE ( 'NONE', ( #4075 ), #1042, .F. ) ;
#18977=CARTESIAN_POINT ( 'NONE',  ( 31.00000000000004263, 68.00000000000000000, -25.99999999999999645 ) ) ;
#19018=FACE_OUTER_BOUND ( 'NONE', #16517, .T. ) ;
#19023=LINE ( 'NONE', #17302, #3648 ) ;
#19024=DIRECTION ( 'NONE',  ( 0.000000000000000000, 0.000000000000000000, 1.000000000000000000 ) ) ;
#19050=CARTESIAN_POINT ( 'NONE',  ( 40.00000000000000000, 68.00000000000000000, 26.00000000000000355 ) ) ;
#19061=VERTEX_POINT ( 'NONE', #1770 ) ;
#19063=ADVANCED_FACE ( 'NONE', ( #6442 ), #9729, .T. ) ;
#19065=VECTOR ( 'NONE', #12405, 1000.000000000000000 ) ;
#19069=CARTESIAN_POINT ( 'NONE',  ( -40.00000000000000000, 68.00000000000000000, 26.00000000000000355 ) ) ;
#19076=DIRECTION ( 'NONE',  ( -0.000000000000000000, -1.000000000000000000, 0.000000000000000000 ) ) ;
#19080=ORIENTED_EDGE ( 'NONE', *, *, #17038, .F. ) ;
#19104=FACE_OUTER_BOUND ( 'NONE', #4745, .T. ) ;
#19106=CARTESIAN_POINT ( 'NONE',  ( -37.00000000000000000, 0.000000000000000000, -22.99999999999999645 ) ) ;
#19109=DIRECTION ( 'NONE',  ( -0.000000000000000000, -1.000000000000000000, -0.000000000000000000 ) ) ;
#19118=VECTOR ( 'NONE', #3360, 1000.000000000000000 ) ;
#19127=ORIENTED_EDGE ( 'NONE', *, *, #12887, .F. ) ;
#19129=VERTEX_POINT ( 'NONE', #14459 ) ;
#19161=AXIS2_PLACEMENT_3D ( 'NONE', #4842, #19024, #12563 ) ;
#19168=EDGE_CURVE ( 'NONE', #1696, #6058, #3647, .T. ) ;
#19201=DIRECTION ( 'NONE',  ( -1.000000000000000000, -0.000000000000000000, -0.000000000000000000 ) ) ;
#19220=DIRECTION ( 'NONE',  ( -0.000000000000000000, -1.000000000000000000, 0.000000000000000000 ) ) ;
#19238=VECTOR ( 'NONE', #19109, 1000.000000000000000 ) ;
#19260=EDGE_CURVE ( 'NONE', #17263, #19061, #4049, .T. ) ;
#19268=ORIENTED_EDGE ( 'NONE', *, *, #12551, .T. ) ;
#19278=LINE ( 'NONE', #397, #15916 ) ;
#19295=DIRECTION ( 'NONE',  ( -1.000000000000000000, 0.000000000000000000, 0.000000000000000000 ) ) ;
#19299=ORIENTED_EDGE ( 'NONE', *, *, #19739, .F. ) ;
#19317=CARTESIAN_POINT ( 'NONE',  ( -31.00000000000003197, 68.00000000000000000, -22.99999999999999645 ) ) ;
#19332=CARTESIAN_POINT ( 'NONE',  ( 25.99999999999999645, 0.000000000000000000, 40.00000000000002132 ) ) ;
#19366=CARTESIAN_POINT ( 'NONE',  ( 26.00000000000001066, 0.000000000000000000, -31.00000000000002487 ) ) ;
#19379=VERTEX_POINT ( 'NONE', #4556 ) ;
#19399=VERTEX_POINT ( 'NONE', #7645 ) ;
#19416=ADVANCED_FACE ( 'NONE', ( #6116 ), #10839, .F. ) ;
#19436=AXIS2_PLACEMENT_3D ( 'NONE', #17738, #8672, #16518 ) ;
#19457=DIRECTION ( 'NONE',  ( 0.000000000000000000, -1.000000000000000000, 0.000000000000000000 ) ) ;
#19492=VECTOR ( 'NONE', #13071, 1000.000000000000000 ) ;
#19512=VERTEX_POINT ( 'NONE', #19366 ) ;
#19550=AXIS2_PLACEMENT_3D ( 'NONE', #5177, #17822, #11448 ) ;
#19565=CARTESIAN_POINT ( 'NONE',  ( -30.99999999999999645, 68.00000000000000000, -30.99999999999999289 ) ) ;
#19573=ORIENTED_EDGE ( 'NONE', *, *, #17957, .T. ) ;
#19621=EDGE_LOOP ( 'NONE', ( #4962, #7527, #19127, #10462 ) ) ;
#19647=AXIS2_PLACEMENT_3D ( 'NONE', #6639, #19076, #17134 ) ;
#19653=CARTESIAN_POINT ( 'NONE',  ( 40.00000000000000000, 68.00000000000000000, 26.00000000000000355 ) ) ;
#19683=EDGE_CURVE ( 'NONE', #12618, #17973, #3133, .T. ) ;
#19685=EDGE_CURVE ( 'NONE', #9045, #12515, #17135, .T. ) ;
#19691=PLANE ( 'NONE',  #6 ) ;
#19692=EDGE_LOOP ( 'NONE', ( #197, #17474, #17339, #13774 ) ) ;
#19739=EDGE_CURVE ( 'NONE', #7970, #19399, #18583, .T. ) ;
#19756=DIRECTION ( 'NONE',  ( -0.000000000000000000, -0.000000000000000000, 1.000000000000000000 ) ) ;
#19763=AXIS2_PLACEMENT_3D ( 'NONE', #15684, #7826, #14316 ) ;
#19775=DIRECTION ( 'NONE',  ( 0.000000000000000000, 0.000000000000000000, -1.000000000000000000 ) ) ;
#19786=CARTESIAN_POINT ( 'NONE',  ( -30.99999999999999289, 68.00000000000000000, 31.00000000000000000 ) ) ;
#19807=EDGE_CURVE ( 'NONE', #13356, #14600, #9822, .T. ) ;
#19808=VECTOR ( 'NONE', #12882, 1000.000000000000000 ) ;
#19824=DIRECTION ( 'NONE',  ( 0.000000000000000000, 0.000000000000000000, -1.000000000000000000 ) ) ;
#19841=CARTESIAN_POINT ( 'NONE',  ( -40.00000000000000000, 68.00000000000000000, 26.00000000000000355 ) ) ;
#19853=CARTESIAN_POINT ( 'NONE',  ( -25.99999999999999645, 0.000000000000000000, -31.00000000000003197 ) ) ;
#19860=VECTOR ( 'NONE', #3747, 1000.000000000000000 ) ;
#19867=VECTOR ( 'NONE', #5957, 1000.000000000000000 ) ;
#19875=VERTEX_POINT ( 'NONE', #2067 ) ;
#19895=ORIENTED_EDGE ( 'NONE', *, *, #10758, .T. ) ;
#19910=LINE ( 'NONE', #4270, #14664 ) ;
#19923=VERTEX_POINT ( 'NONE', #2379 ) ;
#19952=EDGE_CURVE ( 'NONE', #17171, #7013, #11882, .T. ) ;
#20002=DIRECTION ( 'NONE',  ( -0.000000000000000000, -1.000000000000000000, -0.000000000000000000 ) ) ;
#20009=DIRECTION ( 'NONE',  ( -1.000000000000000000, 0.000000000000000000, 0.000000000000000000 ) ) ;
#20042=FACE_OUTER_BOUND ( 'NONE', #2056, .T. ) ;
#20056=DIRECTION ( 'NONE',  ( 0.000000000000000000, 0.000000000000000000, -1.000000000000000000 ) ) ;
#20086=ADVANCED_FACE ( 'NONE', ( #9823 ), #18115, .F. ) ;
#20087=( NAMED_UNIT ( * ) PLANE_ANGLE_UNIT ( ) SI_UNIT ( $, .RADIAN. ) );
#20099=VECTOR ( 'NONE', #20173, 1000.000000000000000 ) ;
#20129=AXIS2_PLACEMENT_3D ( 'NONE', #8618, #3985, #13096 ) ;
#20141=CARTESIAN_POINT ( 'NONE',  ( -22.99999999999999645, 68.00000000000000000, 37.00000000000002132 ) ) ;
#20142=CARTESIAN_POINT ( 'NONE',  ( 23.00000000000000711, 0.000000000000000000, -36.99999999999999289 ) ) ;
#20170=AXIS2_PLACEMENT_3D ( 'NONE', #18135, #5492, #19775 ) ;
#20173=DIRECTION ( 'NONE',  ( 0.000000000000000000, 0.000000000000000000, -1.000000000000000000 ) ) ;
#20174=EDGE_CURVE ( 'NONE', #3145, #19061, #15364, .T. ) ;
#20180=EDGE_LOOP ( 'NONE', ( #18809, #18405, #5504, #15667 ) ) ;
#20203=ORIENTED_EDGE ( 'NONE', *, *, #300, .F. ) ;
#20204=FACE_OUTER_BOUND ( 'NONE', #20180, .T. ) ;
#20220=VECTOR ( 'NONE', #9977, 1000.000000000000000 ) ;
#20222=CARTESIAN_POINT ( 'NONE',  ( -25.99999999999999645, 68.00000000000000000, 40.00000000000002132 ) ) ;
#20258=CARTESIAN_POINT ( 'NONE',  ( -31.00000000000003197, 68.00000000000000000, 26.00000000000000355 ) ) ;
#20270=VECTOR ( 'NONE', #8649, 1000.000000000000000 ) ;
#20314=DIRECTION ( 'NONE',  ( 0.000000000000000000, 0.000000000000000000, 1.000000000000000000 ) ) ;
#20355=VERTEX_POINT ( 'NONE', #78 ) ;
ENDSEC;
END-ISO-10303-21;
